ISO-10303-21;
HEADER;
FILE_DESCRIPTION (('STEP AP214'),
    '1' );
FILE_NAME ('short pitch roller chain wheel_s_iso_Chain wheel ISO - 12Z 05B-1 --12SA8.0N.step',
    '2026-10-31T03:41:51',
    ( '' ),
    ( '' ),
    'SwSTEP 2.0',
    'SolidWorks 2026',
    '' );
FILE_SCHEMA (( 'AUTOMOTIVE_DESIGN' ));
ENDSEC;

DATA;
#6=EDGE_LOOP ( 'NONE', ( #14602, #6535, #10108, #15176, #740, #8650, #3309 ) ) ;
#7=DIRECTION ( 'NONE',  ( -1.000000000000000000, -0.000000000000000000, -0.000000000000000000 ) ) ;
#8=CARTESIAN_POINT ( 'NONE',  ( 1.749999999999999778, 0.000000000000000000, 0.000000000000000000 ) ) ;
#20=CARTESIAN_POINT ( 'NONE',  ( 0.02531912748631424959, 14.46287784598617243, 2.311161484776605324 ) ) ;
#28=DIRECTION ( 'NONE',  ( -1.000000000000000000, 0.000000000000000000, 0.000000000000000000 ) ) ;
#33=CARTESIAN_POINT ( 'NONE',  ( 0.02531912748606228100, 5.229914364928351489, 13.68080036884350292 ) ) ;
#35=VECTOR ( 'NONE', #190, 1000.000000000000000 ) ;
#41=CARTESIAN_POINT ( 'NONE',  ( 2.597943782557557313, 12.05486625177586113, -10.28947301956269733 ) ) ;
#46=EDGE_CURVE ( 'NONE', #11802, #6223, #12333, .T. ) ;
#53=B_SPLINE_CURVE_WITH_KNOTS ( 'NONE', 3,
 ( #7309, #10834, #290, #4708, #9377, #14064, #7077, #10905 ),
 .UNSPECIFIED., .F., .F.,
 ( 4, 2, 2, 4 ),
 ( 1.984117563342701228E-07, 0.001895214258086351869, 0.002842722181251365696, 0.003790230104416379524 ),
 .UNSPECIFIED. ) ;
#55=EDGE_LOOP ( 'NONE', ( #13749, #2858, #11395, #485, #2000, #143, #1377, #4123 ) ) ;
#63=CARTESIAN_POINT ( 'NONE',  ( 2.021362784118872380, 12.71987259277435101, 11.98841295390602291 ) ) ;
#66=ADVANCED_FACE ( 'NONE', ( #13569 ), #14807, .T. ) ;
#67=PRODUCT_DEFINITION_FORMATION_WITH_SPECIFIED_SOURCE ( 'ANY', '', #14008, .NOT_KNOWN. ) ;
#77=CARTESIAN_POINT ( 'NONE',  ( 1.394999999999998685, -17.29145405592685592, -4.835383649608655077 ) ) ;
#81=LINE ( 'NONE', #4807, #9670 ) ;
#87=DIRECTION ( 'NONE',  ( -1.000000000000000000, 0.000000000000000000, -0.000000000000000000 ) ) ;
#90=CARTESIAN_POINT ( 'NONE',  ( 0.07473575470096445461, -11.74839219818081482, -9.749517823374134196 ) ) ;
#110=ORIENTED_EDGE ( 'NONE', *, *, #7513, .T. ) ;
#111=CARTESIAN_POINT ( 'NONE',  ( 1.749999999999999778, 17.39253030560841395, -4.458161950358560333 ) ) ;
#113=EDGE_CURVE ( 'NONE', #13456, #5828, #10676, .T. ) ;
#114=CARTESIAN_POINT ( 'NONE',  ( 0.5537796329733287726, 5.139875429511856275, 16.15122426806991385 ) ) ;
#115=CARTESIAN_POINT ( 'NONE',  ( 2.740003299868483566, 9.490919315500294218, -11.55877992729655368 ) ) ;
#119=CIRCLE ( 'NONE', #7473, 14.01039946648074341 ) ;
#130=EDGE_CURVE ( 'NONE', #2515, #5688, #11223, .T. ) ;
#132=VERTEX_POINT ( 'NONE', #20 ) ;
#142=AXIS2_PLACEMENT_3D ( 'NONE', #6608, #14906, #1917 ) ;
#143=ORIENTED_EDGE ( 'NONE', *, *, #12762, .T. ) ;
#150=EDGE_LOOP ( 'NONE', ( #5698, #6923, #12784, #4888 ) ) ;
#152=CARTESIAN_POINT ( 'NONE',  ( 1.039999999999996261, -17.29145405592685592, -4.835383649608655077 ) ) ;
#157=VECTOR ( 'NONE', #9903, 1000.000000000000000 ) ;
#159=VERTEX_POINT ( 'NONE', #10494 ) ;
#165=DIRECTION ( 'NONE',  ( 0.000000000000000000, 0.8660254037844327124, 0.5000000000000104361 ) ) ;
#171=CARTESIAN_POINT ( 'NONE',  ( 1.039999999999997371, 4.458161950358744186, -17.39253030560836777 ) ) ;
#173=CIRCLE ( 'NONE', #4631, 14.01039946648074341 ) ;
#176=EDGE_LOOP ( 'NONE', ( #1544, #7262 ) ) ;
#182=CARTESIAN_POINT ( 'NONE',  ( 2.782672467460656218, 14.24942254254689189, 2.217238903388611071 ) ) ;
#184=DIRECTION ( 'NONE',  ( -1.000000000000000000, -0.000000000000000000, -0.000000000000000000 ) ) ;
#190=DIRECTION ( 'NONE',  ( 1.000000000000000000, -0.000000000000000000, -0.000000000000000000 ) ) ;
#191=DIRECTION ( 'NONE',  ( -1.000000000000000000, 0.000000000000000000, 0.000000000000000000 ) ) ;
#195=ORIENTED_EDGE ( 'NONE', *, *, #10486, .F. ) ;
#199=CARTESIAN_POINT ( 'NONE',  ( 0.07473581742173406040, 5.299647274067100788, 14.31752701692938778 ) ) ;
#200=CARTESIAN_POINT ( 'NONE',  ( 2.246812931352481613, 11.42270873787310315, -12.54666350726111901 ) ) ;
#204=FACE_OUTER_BOUND ( 'NONE', #6, .T. ) ;
#205=DIRECTION ( 'NONE',  ( 0.000000000000000000, 0.000000000000000000, 1.000000000000000000 ) ) ;
#207=DIRECTION ( 'NONE',  ( -1.000000000000000000, -0.000000000000000000, 0.000000000000000000 ) ) ;
#208=CARTESIAN_POINT ( 'NONE',  ( 0.07473575470096512074, 9.749517823374169723, -11.74839219818077929 ) ) ;
#210=FACE_OUTER_BOUND ( 'NONE', #11250, .T. ) ;
#212=VERTEX_POINT ( 'NONE', #10569 ) ;
#213=ORIENTED_EDGE ( 'NONE', *, *, #12762, .F. ) ;
#218=CARTESIAN_POINT ( 'NONE',  ( 2.790000000000009805, 5.211150952915548196, -13.21889893246969905 ) ) ;
#219=DIRECTION ( 'NONE',  ( -1.000000000000000000, -0.000000000000000000, -0.000000000000000000 ) ) ;
#222=DIRECTION ( 'NONE',  ( -1.000000000000000000, -0.000000000000000000, -0.000000000000000000 ) ) ;
#225=ADVANCED_FACE ( 'NONE', ( #6882 ), #11561, .F. ) ;
#228=VERTEX_POINT ( 'NONE', #7180 ) ;
#236=ADVANCED_FACE ( 'NONE', ( #12247, #14409 ), #3875, .F. ) ;
#238=CARTESIAN_POINT ( 'NONE',  ( 2.740003288479521348, -14.75565684666125144, -2.439987328297124947 ) ) ;
#242=B_SPLINE_CURVE_WITH_KNOTS ( 'NONE', 3,
 ( #7619, #12222, #12296, #11068, #11983, #9993, #527, #1623 ),
 .UNSPECIFIED., .F., .F.,
 ( 4, 2, 2, 4 ),
 ( 2.445728210258510103E-07, 0.001895260649874687441, 0.002842768688401517505, 0.003790276726928347353 ),
 .UNSPECIFIED. ) ;
#256=PRODUCT_DEFINITION_SHAPE ( 'NONE', 'NONE',  #13870 ) ;
#258=CARTESIAN_POINT ( 'NONE',  ( 0.02531912748464848137, 2.311161484776556030, 14.46287784598618309 ) ) ;
#262=CARTESIAN_POINT ( 'NONE',  ( 2.337784062669523877, -3.429166897524313029, -16.32199768300083420 ) ) ;
#263=DIRECTION ( 'NONE',  ( 0.000000000000000000, 0.000000000000000000, -1.000000000000000000 ) ) ;
#266=EDGE_LOOP ( 'NONE', ( #5592, #13272, #13522, #7221 ) ) ;
#267=VECTOR ( 'NONE', #3874, 1000.000000000000000 ) ;
#282=DIRECTION ( 'NONE',  ( 0.000000000000000000, 0.000000000000000000, 1.000000000000000000 ) ) ;
#283=CARTESIAN_POINT ( 'NONE',  ( 2.789999999999999147, 3.120158876139233595, -14.59528211759998939 ) ) ;
#288=ORIENTED_EDGE ( 'NONE', *, *, #5024, .T. ) ;
#290=CARTESIAN_POINT ( 'NONE',  ( 0.1920564340659368652, -5.295083827234610574, -14.93837896275555721 ) ) ;
#293=CARTESIAN_POINT ( 'NONE',  ( 2.782650494170371580, 5.204557061642474558, -13.44926448535260377 ) ) ;
#294=DIRECTION ( 'NONE',  ( -1.000000000000000000, -0.000000000000000000, -0.000000000000000000 ) ) ;
#299=B_SPLINE_CURVE_WITH_KNOTS ( 'NONE', 3,
 ( #2873, #12317, #14722, #1958 ),
 .UNSPECIFIED., .F., .F.,
 ( 4, 4 ),
 ( 0.005540500595652399218, 0.005814376014856854034 ),
 .UNSPECIFIED. ) ;
#300=LINE ( 'NONE', #8227, #4591 ) ;
#304=B_SPLINE_CURVE_WITH_KNOTS ( 'NONE', 3,
 ( #13132, #218, #293, #11828 ),
 .UNSPECIFIED., .F., .F.,
 ( 4, 4 ),
 ( 0.005123742438166219160, 0.005814376014856852300 ),
 .UNSPECIFIED. ) ;
#308=ORIENTED_EDGE ( 'NONE', *, *, #8675, .F. ) ;
#309=EDGE_CURVE ( 'NONE', #2455, #13045, #11550, .T. ) ;
#312=DIRECTION ( 'NONE',  ( 0.000000000000000000, 0.000000000000000000, 1.000000000000000000 ) ) ;
#319=ORIENTED_EDGE ( 'NONE', *, *, #11799, .F. ) ;
#320=DIRECTION ( 'NONE',  ( 0.000000000000000000, 0.000000000000000000, 1.000000000000000000 ) ) ;
#327=B_SPLINE_CURVE_WITH_KNOTS ( 'NONE', 3,
 ( #9952, #1804, #5582, #14799 ),
 .UNSPECIFIED., .F., .F.,
 ( 4, 4 ),
 ( 0.005123713096549426665, 0.005814346476695865691 ),
 .UNSPECIFIED. ) ;
#329=FACE_OUTER_BOUND ( 'NONE', #10914, .T. ) ;
#341=ORIENTED_EDGE ( 'NONE', *, *, #8187, .F. ) ;
#342=ORIENTED_EDGE ( 'NONE', *, *, #10454, .F. ) ;
#343=CIRCLE ( 'NONE', #11635, 2.524999999999998579 ) ;
#349=CYLINDRICAL_SURFACE ( 'NONE', #13438, 4.000000000000000000 ) ;
#357=FACE_OUTER_BOUND ( 'NONE', #5702, .T. ) ;
#362=CARTESIAN_POINT ( 'NONE',  ( 0.000000000000000000, -5.249430348645841349, 12.98979500319692626 ) ) ;
#365=CARTESIAN_POINT ( 'NONE',  ( 0.04999670013151490816, -11.55877992729671888, 9.490919315500097042 ) ) ;
#367=VERTEX_POINT ( 'NONE', #13477 ) ;
#369=ORIENTED_EDGE ( 'NONE', *, *, #4930, .F. ) ;
#373=CARTESIAN_POINT ( 'NONE',  ( 0.07473579423048590242, -15.04916547791952119, -2.569134216959054751 ) ) ;
#374=CARTESIAN_POINT ( 'NONE',  ( 2.764680872513207266, -9.232963481057685939, -11.36963888406697087 ) ) ;
#381=SURFACE_SIDE_STYLE ('',( #533 ) ) ;
#386=EDGE_CURVE ( 'NONE', #14639, #7731, #1893, .T. ) ;
#388=B_SPLINE_CURVE_WITH_KNOTS ( 'NONE', 3,
 ( #10440, #12588, #1999, #9069 ),
 .UNSPECIFIED., .F., .F.,
 ( 4, 4 ),
 ( 1.988537749986050620E-07, 0.0006916721208754040336 ),
 .UNSPECIFIED. ) ;
#391=UNCERTAINTY_MEASURE_WITH_UNIT (LENGTH_MEASURE( 1.000000000000000082E-05 ), #9778, 'distance_accuracy_value', 'NONE');
#393=VERTEX_POINT ( 'NONE', #7047 ) ;
#395=CARTESIAN_POINT ( 'NONE',  ( 0.000000000000000000, -5.249430348645841349, 12.98979500319692626 ) ) ;
#397=TOROIDAL_SURFACE ( 'NONE', #10724, 14.01039946648073986, 8.000000000000000000 ) ;
#399=EDGE_CURVE ( 'NONE', #5499, #5314, #14702, .T. ) ;
#404=CARTESIAN_POINT ( 'NONE',  ( 1.039999999999997593, -4.458161950358380032, -17.39253030560846369 ) ) ;
#406=VERTEX_POINT ( 'NONE', #13971 ) ;
#407=DIRECTION ( 'NONE',  ( -1.000000000000000000, -0.000000000000000000, 0.000000000000000000 ) ) ;
#419=ORIENTED_EDGE ( 'NONE', *, *, #12361, .F. ) ;
#429=DIRECTION ( 'NONE',  ( 0.000000000000000000, 0.000000000000000000, 1.000000000000000000 ) ) ;
#430=ORIENTED_EDGE ( 'NONE', *, *, #3464, .T. ) ;
#435=ORIENTED_EDGE ( 'NONE', *, *, #10644, .T. ) ;
#444=CARTESIAN_POINT ( 'NONE',  ( 2.508169719062756986, -10.58084377126631814, 12.18203740414262803 ) ) ;
#451=CARTESIAN_POINT ( 'NONE',  ( 2.782672435525938237, 9.044896821682357313, -11.23174270417319676 ) ) ;
#452=CARTESIAN_POINT ( 'NONE',  ( 2.764680872515352661, -2.311161484776655950, 14.46287784598616355 ) ) ;
#463=ADVANCED_FACE ( 'NONE', ( #9503 ), #15129, .T. ) ;
#464=PRESENTATION_STYLE_ASSIGNMENT (( #1775 ) ) ;
#465=ORIENTED_EDGE ( 'NONE', *, *, #12135, .F. ) ;
#468=CARTESIAN_POINT ( 'NONE',  ( 1.039999999999996261, -4.835383649608352208, -17.29145405592693763 ) ) ;
#472=CARTESIAN_POINT ( 'NONE',  ( -10.00000000000000000, 0.000000000000000000, 0.000000000000000000 ) ) ;
#476=ADVANCED_BREP_SHAPE_REPRESENTATION ( '', ( #9040, #1376 ), #13900 ) ;
#477=CIRCLE ( 'NONE', #9084, 17.95481323787947403 ) ;
#484=VERTEX_POINT ( 'NONE', #9353 ) ;
#485=ORIENTED_EDGE ( 'NONE', *, *, #6558, .T. ) ;
#486=CIRCLE ( 'NONE', #11774, 14.01039946648074341 ) ;
#488=CYLINDRICAL_SURFACE ( 'NONE', #10200, 2.524999999999999467 ) ;
#489=CARTESIAN_POINT ( 'NONE',  ( 2.789999999999999147, 8.624777288397799779, 11.04103753892274753 ) ) ;
#493=FACE_OUTER_BOUND ( 'NONE', #2373, .T. ) ;
#496=ORIENTED_EDGE ( 'NONE', *, *, #10416, .F. ) ;
#498=B_SPLINE_CURVE_WITH_KNOTS ( 'NONE', 3,
 ( #4619, #8065, #4302, #10295 ),
 .UNSPECIFIED., .F., .F.,
 ( 4, 4 ),
 ( 2.159563976372916968E-07, 0.0006916893629248549880 ),
 .UNSPECIFIED. ) ;
#500=DIRECTION ( 'NONE',  ( 0.000000000000000000, 0.000000000000000000, 1.000000000000000000 ) ) ;
#504=CARTESIAN_POINT ( 'NONE',  ( 1.885839510111768869, 4.928563447326528291, -17.01651022436359284 ) ) ;
#506=CARTESIAN_POINT ( 'NONE',  ( 1.039999999999997371, 4.458161950358744186, -17.39253030560836777 ) ) ;
#508=ORIENTED_EDGE ( 'NONE', *, *, #8414, .T. ) ;
#510=CARTESIAN_POINT ( 'NONE',  ( -10.00000000000000000, 0.000000000000000000, 0.000000000000000000 ) ) ;
#515=CARTESIAN_POINT ( 'NONE',  ( 0.5431871198829556491, -16.57708379306446389, 3.619024283482010329 ) ) ;
#516=VERTEX_POINT ( 'NONE', #10650 ) ;
#519=CARTESIAN_POINT ( 'NONE',  ( 2.790000000000061764, 5.211197193340692202, 13.21862218141517786 ) ) ;
#527=CARTESIAN_POINT ( 'NONE',  ( 1.885839528871393611, 12.27244837507612729, 12.77651625388903511 ) ) ;
#528=EDGE_LOOP ( 'NONE', ( #12850, #12024, #5679, #2607, #4048, #7554, #5899 ) ) ;
#530=B_SPLINE_CURVE_WITH_KNOTS ( 'NONE', 3,
 ( #8479, #3720, #8565, #2657 ),
 .UNSPECIFIED., .F., .F.,
 ( 4, 4 ),
 ( 0.005123695899043905454, 0.005814329666474870109 ),
 .UNSPECIFIED. ) ;
#533=SURFACE_STYLE_FILL_AREA ( #5103 ) ;
#535=ORIENTED_EDGE ( 'NONE', *, *, #12540, .F. ) ;
#539=ADVANCED_FACE ( 'NONE', ( #8645 ), #1738, .T. ) ;
#540=EDGE_CURVE ( 'NONE', #1061, #7151, #11199, .T. ) ;
#544=DIRECTION ( 'NONE',  ( -1.000000000000000000, 0.000000000000000000, 0.000000000000000000 ) ) ;
#553=CARTESIAN_POINT ( 'NONE',  ( 0.5537796329733288836, 16.15122426806996003, -5.139875429511683969 ) ) ;
#556=ORIENTED_EDGE ( 'NONE', *, *, #12002, .F. ) ;
#563=CARTESIAN_POINT ( 'NONE',  ( 2.236220367026669376, -5.139875429511969962, 16.15122426806987121 ) ) ;
#579=CARTESIAN_POINT ( 'NONE',  ( 0.000000000000000000, 11.04103753892271733, 8.624777288397844188 ) ) ;
#581=CARTESIAN_POINT ( 'NONE',  ( 0.4522159468065706789, -11.13074453164212407, 12.42068120944077236 ) ) ;
#584=ORIENTED_EDGE ( 'NONE', *, *, #6185, .F. ) ;
#588=DIRECTION ( 'NONE',  ( 0.000000000000000000, 0.000000000000000000, 1.000000000000000000 ) ) ;
#590=ORIENTED_EDGE ( 'NONE', *, *, #386, .F. ) ;
#592=AXIS2_PLACEMENT_3D ( 'NONE', #283, #11969, #7217 ) ;
#599=FACE_OUTER_BOUND ( 'NONE', #10458, .T. ) ;
#606=DIRECTION ( 'NONE',  ( 0.000000000000000000, 0.000000000000000000, 1.000000000000000000 ) ) ;
#617=ORIENTED_EDGE ( 'NONE', *, *, #13935, .T. ) ;
#620=CARTESIAN_POINT ( 'NONE',  ( 2.790000000000061764, -11.12234047011184046, -8.842064619038639606 ) ) ;
#624=DIRECTION ( 'NONE',  ( 0.000000000000000000, 0.000000000000000000, 1.000000000000000000 ) ) ;
#625=AXIS2_PLACEMENT_3D ( 'NONE', #472, #6400, #14629 ) ;
#627=CARTESIAN_POINT ( 'NONE',  ( 0.04914328897885022335, 13.98777112126087552, 5.263533129984400816 ) ) ;
#628=CARTESIAN_POINT ( 'NONE',  ( 2.789999999999999147, 13.40591150984237245, -5.214906618939568084 ) ) ;
#630=EDGE_CURVE ( 'NONE', #7999, #6679, #7832, .T. ) ;
#631=B_SPLINE_CURVE_WITH_KNOTS ( 'NONE', 3,
 ( #5423, #4332, #9013, #1871, #10017, #14718, #14636, #6404 ),
 .UNSPECIFIED., .F., .F.,
 ( 4, 2, 2, 4 ),
 ( 4.663089340421306733E-07, 0.001440500229357228462, 0.002160517189568826168, 0.002880534149780423873 ),
 .UNSPECIFIED. ) ;
#639=ORIENTED_EDGE ( 'NONE', *, *, #11028, .T. ) ;
#643=DIRECTION ( 'NONE',  ( 0.000000000000000000, 0.5000000000000071054, -0.8660254037844345998 ) ) ;
#647=AXIS2_PLACEMENT_3D ( 'NONE', #1933, #12597, #3237 ) ;
#656=ORIENTED_EDGE ( 'NONE', *, *, #11404, .T. ) ;
#660=EDGE_CURVE ( 'NONE', #7996, #4412, #13722, .T. ) ;
#661=CIRCLE ( 'NONE', #7295, 2.524999999999999023 ) ;
#669=AXIS2_PLACEMENT_3D ( 'NONE', #2925, #13445, #8902 ) ;
#676=CARTESIAN_POINT ( 'NONE',  ( 2.781248467066446572, 13.40591150985955871, -5.214906618939568972 ) ) ;
#687=CARTESIAN_POINT ( 'NONE',  ( 0.007349557670560538138, -11.23191127083857133, -9.045126717605896260 ) ) ;
#688=CARTESIAN_POINT ( 'NONE',  ( 0.5537796532149691364, -16.55730827443878539, -3.624349476775370782 ) ) ;
#692=CARTESIAN_POINT ( 'NONE',  ( 2.789999999999999147, -7.739906618939802918, 13.40591150984224100 ) ) ;
#726=ADVANCED_FACE ( 'NONE', ( #10666 ), #6857, .T. ) ;
#728=B_SPLINE_CURVE_WITH_KNOTS ( 'NONE', 3,
 ( #579, #5152, #8730, #13575 ),
 .UNSPECIFIED., .F., .F.,
 ( 4, 4 ),
 ( 0.005123695899043910658, 0.005814329666474866640 ),
 .UNSPECIFIED. ) ;
#740=ORIENTED_EDGE ( 'NONE', *, *, #1383, .F. ) ;
#743=ORIENTED_EDGE ( 'NONE', *, *, #8518, .T. ) ;
#749=CARTESIAN_POINT ( 'NONE',  ( 50.00050000000000239, 4.898587196589412829E-16, -4.000000000000000000 ) ) ;
#754=CARTESIAN_POINT ( 'NONE',  ( 2.764680872515352217, 2.311161484776756758, -14.46287784598614756 ) ) ;
#757=B_SPLINE_CURVE_WITH_KNOTS ( 'NONE', 3,
 ( #2681, #12103, #1282, #5975 ),
 .UNSPECIFIED., .F., .F.,
 ( 4, 4 ),
 ( 0.005123742438166214823, 0.005814376014856804595 ),
 .UNSPECIFIED. ) ;
#762=ORIENTED_EDGE ( 'NONE', *, *, #12185, .F. ) ;
#765=CARTESIAN_POINT ( 'NONE',  ( 2.764680872515352217, 2.311161484776756758, -14.46287784598614756 ) ) ;
#768=CYLINDRICAL_SURFACE ( 'NONE', #12984, 8.400000000000000355 ) ;
#777=DIRECTION ( 'NONE',  ( 0.000000000000000000, 0.000000000000000000, 1.000000000000000000 ) ) ;
#783=DIRECTION ( 'NONE',  ( 0.000000000000000000, 0.8660254037844327124, 0.5000000000000104361 ) ) ;
#786=DIRECTION ( 'NONE',  ( -1.000000000000000000, -0.000000000000000000, -0.000000000000000000 ) ) ;
#790=EDGE_CURVE ( 'NONE', #6334, #6870, #7715, .T. ) ;
#798=CARTESIAN_POINT ( 'NONE',  ( 1.039999999999998037, -4.835383649608592904, 17.29145405592687368 ) ) ;
#799=VERTEX_POINT ( 'NONE', #7292 ) ;
#812=CYLINDRICAL_SURFACE ( 'NONE', #5102, 4.000000000000000000 ) ;
#822=ADVANCED_FACE ( 'NONE', ( #357 ), #14285, .F. ) ;
#827=DIRECTION ( 'NONE',  ( -1.000000000000000000, -0.000000000000000000, 0.000000000000000000 ) ) ;
#828=LINE ( 'NONE', #2218, #7522 ) ;
#829=ORIENTED_EDGE ( 'NONE', *, *, #13134, .T. ) ;
#831=B_SPLINE_CURVE_WITH_KNOTS ( 'NONE', 3,
 ( #2977, #1985, #13577, #581, #6511, #13738, #7665, #6669 ),
 .UNSPECIFIED., .F., .F.,
 ( 4, 2, 2, 4 ),
 ( 2.445728210282456254E-07, 0.001895260649874687007, 0.002842768688401519240, 0.003790276726928351256 ),
 .UNSPECIFIED. ) ;
#838=FACE_OUTER_BOUND ( 'NONE', #3603, .T. ) ;
#840=EDGE_CURVE ( 'NONE', #14323, #9602, #11010, .T. ) ;
#841=AXIS2_PLACEMENT_3D ( 'NONE', #8446, #219, #11761 ) ;
#844=FACE_OUTER_BOUND ( 'NONE', #4156, .T. ) ;
#849=ORIENTED_EDGE ( 'NONE', *, *, #4788, .T. ) ;
#853=CARTESIAN_POINT ( 'NONE',  ( 2.597943782557557313, -12.05486625177578830, 10.28947301956278082 ) ) ;
#871=ORIENTED_EDGE ( 'NONE', *, *, #5784, .F. ) ;
#874=ORIENTED_EDGE ( 'NONE', *, *, #399, .F. ) ;
#882=CARTESIAN_POINT ( 'NONE',  ( 0.02531912748464848137, 2.311161484776556030, 14.46287784598618309 ) ) ;
#884=ORIENTED_EDGE ( 'NONE', *, *, #9768, .T. ) ;
#889=B_SPLINE_CURVE_WITH_KNOTS ( 'NONE', 3,
 ( #3132, #1814, #6729, #14972 ),
 .UNSPECIFIED., .F., .F.,
 ( 4, 4 ),
 ( 2.159563976372915910E-07, 0.0006916893629248579154 ),
 .UNSPECIFIED. ) ;
#890=LINE ( 'NONE', #749, #1286 ) ;
#891=AXIS2_PLACEMENT_3D ( 'NONE', #7418, #1421, #10719 ) ;
#905=AXIS2_PLACEMENT_3D ( 'NONE', #10833, #8147, #8369 ) ;
#907=AXIS2_PLACEMENT_3D ( 'NONE', #8503, #6206, #13195 ) ;
#935=CARTESIAN_POINT ( 'NONE',  ( 2.697960317788776763, -5.280991956247018670, -14.31435947614547821 ) ) ;
#936=EDGE_CURVE ( 'NONE', #4803, #367, #12085, .T. ) ;
#940=CARTESIAN_POINT ( 'NONE',  ( 2.781248467067199748, -13.40591150984217705, -5.214906618939849636 ) ) ;
#945=AXIS2_PLACEMENT_3D ( 'NONE', #5676, #3219, #1827 ) ;
#946=ORIENTED_EDGE ( 'NONE', *, *, #10600, .T. ) ;
#957=TOROIDAL_SURFACE ( 'NONE', #14218, 14.01039946648073986, 8.000000000000000000 ) ;
#960=VERTEX_POINT ( 'NONE', #10398 ) ;
#967=CARTESIAN_POINT ( 'NONE',  ( 2.789999999999999147, -5.404747904883309660E-14, 15.47981323787947794 ) ) ;
#971=CARTESIAN_POINT ( 'NONE',  ( 2.789999999999999147, 13.87420763704361093, 1.948757464274220697 ) ) ;
#978=CARTESIAN_POINT ( 'NONE',  ( 0.02531912748631078014, -2.311161484776655950, 14.46287784598616355 ) ) ;
#985=CARTESIAN_POINT ( 'NONE',  ( 0.2818303916520940589, 5.259531939870414341, -15.25429862889476240 ) ) ;
#992=B_SPLINE_CURVE_WITH_KNOTS ( 'NONE', 3,
 ( #4190, #6566, #9941, #3027, #5427, #7643, #7714, #5497 ),
 .UNSPECIFIED., .F., .F.,
 ( 4, 2, 2, 4 ),
 ( 4.663089536290197543E-07, 0.001898630414085408650, 0.002847712466651295803, 0.003796794519217183174 ),
 .UNSPECIFIED. ) ;
#1001=B_SPLINE_CURVE_WITH_KNOTS ( 'NONE', 3,
 ( #1140, #4615, #14043, #11654 ),
 .UNSPECIFIED., .F., .F.,
 ( 4, 4 ),
 ( 0.0002742066915202718549, 0.0006916721208754016484 ),
 .UNSPECIFIED. ) ;
#1004=ADVANCED_FACE ( 'NONE', ( #1031 ), #8438, .T. ) ;
#1007=VERTEX_POINT ( 'NONE', #9258 ) ;
#1009=FACE_OUTER_BOUND ( 'NONE', #10518, .T. ) ;
#1010=CARTESIAN_POINT ( 'NONE',  ( 2.508169608347903257, -5.259531939870091932, -15.25429862889487076 ) ) ;
#1021=B_SPLINE_CURVE_WITH_KNOTS ( 'NONE', 3,
 ( #9744, #3909, #1597, #13271, #2751, #7443 ),
 .UNSPECIFIED., .F., .F.,
 ( 4, 2, 4 ),
 ( 0.0009182716802120147702, 0.002354250892314196063, 0.003790230104416377789 ),
 .UNSPECIFIED. ) ;
#1028=B_SPLINE_CURVE_WITH_KNOTS ( 'NONE', 3,
 ( #7224, #7076, #7152, #5858, #10543, #6075 ),
 .UNSPECIFIED., .F., .F.,
 ( 4, 2, 4 ),
 ( 0.0009182716802119580664, 0.002354250892314169608, 0.003790230104416381259 ),
 .UNSPECIFIED. ) ;
#1031=FACE_OUTER_BOUND ( 'NONE', #13641, .T. ) ;
#1032=CARTESIAN_POINT ( 'NONE',  ( 0.000000000000000000, -8.624777288397730501, -11.04103753892280615 ) ) ;
#1034=CARTESIAN_POINT ( 'NONE',  ( 1.955868201400819517, -16.87476974924773288, 4.976599981640283943 ) ) ;
#1054=DIRECTION ( 'NONE',  ( -1.000000000000000000, -0.000000000000000000, 0.000000000000000000 ) ) ;
#1061=VERTEX_POINT ( 'NONE', #2412 ) ;
#1066=CARTESIAN_POINT ( 'NONE',  ( -10.00000000000000000, 0.000000000000000000, 0.000000000000000000 ) ) ;
#1068=DIRECTION ( 'NONE',  ( 0.000000000000000000, 0.000000000000000000, 1.000000000000000000 ) ) ;
#1071=VERTEX_POINT ( 'NONE', #1409 ) ;
#1073=DIRECTION ( 'NONE',  ( -1.000000000000000000, 0.000000000000000000, -0.000000000000000000 ) ) ;
#1074=ADVANCED_FACE ( 'NONE', ( #9706 ), #13240, .F. ) ;
#1077=ORIENTED_EDGE ( 'NONE', *, *, #7513, .F. ) ;
#1081=FACE_OUTER_BOUND ( 'NONE', #1333, .T. ) ;
#1082=CLOSED_SHELL ( 'NONE', ( #13807, #8527, #4660, #7191, #6991, #11941, #10621, #225, #1968, #4967, #10970, #9272, #726, #4847, #5728, #6700, #3383, #3396, #7586, #1751, #12998, #2428, #2056, #9460, #10685, #12723, #3621, #9453, #10423, #11678, #5875, #5344, #7238, #9097, #1004, #1780, #1937, #11299, #9087, #13708, #5635, #2775, #13518, #5185, #236, #6070, #463, #12791, #1074, #11354, #10231, #10765, #4415, #3764, #5637, #14346, #11847, #4400, #4712, #15088, #3270, #822, #8033, #10158, #4186, #66, #12267, #2450, #11769, #1118, #7211, #9365, #3656, #9856, #539, #13279, #6798, #5189, #10942, #5043, #10869, #6169, #14947 ) ) ;
#1083=CARTESIAN_POINT ( 'NONE',  ( 0.04999670013151481102, -9.490919315500054410, -11.55877992729675263 ) ) ;
#1086=CARTESIAN_POINT ( 'NONE',  ( 1.039999999999997593, -4.458161950358380032, -17.39253030560846369 ) ) ;
#1106=CARTESIAN_POINT ( 'NONE',  ( 2.246812850058911071, 16.16568790143448453, -5.154374911958746530 ) ) ;
#1108=CARTESIAN_POINT ( 'NONE',  ( 1.039999999999996261, 12.83329210556831512, 12.55714665599991697 ) ) ;
#1118=ADVANCED_FACE ( 'NONE', ( #8466 ), #7171, .T. ) ;
#1119=CARTESIAN_POINT ( 'NONE',  ( 0.000000000000000000, 8.624777288397959651, -11.04103753892262674 ) ) ;
#1121=EDGE_CURVE ( 'NONE', #2246, #12653, #6172, .T. ) ;
#1124=FACE_OUTER_BOUND ( 'NONE', #2162, .T. ) ;
#1128=AXIS2_PLACEMENT_3D ( 'NONE', #1483, #12308, #10849 ) ;
#1132=CARTESIAN_POINT ( 'NONE',  ( 1.749999999999999778, 0.000000000000000000, 0.000000000000000000 ) ) ;
#1138=CARTESIAN_POINT ( 'NONE',  ( 2.789999999999999147, -7.739906618939614624, -10.88091150984234545 ) ) ;
#1140=CARTESIAN_POINT ( 'NONE',  ( 0.008751532933531189218, -13.40591150985895297, -5.214906618939850524 ) ) ;
#1143=STYLED_ITEM ( 'NONE', ( #464 ), #476 ) ;
#1148=CARTESIAN_POINT ( 'NONE',  ( 2.789999999999999147, 0.000000000000000000, 0.000000000000000000 ) ) ;
#1152=CARTESIAN_POINT ( 'NONE',  ( 0.7795480763126773072, 11.98750039041511961, -12.70439593876648132 ) ) ;
#1156=EDGE_CURVE ( 'NONE', #516, #5499, #14365, .T. ) ;
#1164=CARTESIAN_POINT ( 'NONE',  ( 0.007327513813774171221, 5.204526028255878067, -13.44898112152233338 ) ) ;
#1169=ORIENTED_EDGE ( 'NONE', *, *, #8068, .F. ) ;
#1170=STYLED_ITEM('',(#15265),#9040);
#1183=EDGE_CURVE ( 'NONE', #12755, #132, #7011, .T. ) ;
#1184=AXIS2_PLACEMENT_3D ( 'NONE', #13289, #8751, #6304 ) ;
#1186=DIRECTION ( 'NONE',  ( -1.000000000000000000, -0.000000000000000000, -0.000000000000000000 ) ) ;
#1187=CARTESIAN_POINT ( 'NONE',  ( 2.429628795537856156, -15.53862542373106237, 5.230001598524554929 ) ) ;
#1194=EDGE_CURVE ( 'NONE', #4401, #3473, #10561, .T. ) ;
#1196=EDGE_LOOP ( 'NONE', ( #110, #1509, #11563, #8866 ) ) ;
#1197=CARTESIAN_POINT ( 'NONE',  ( 0.2076373605413187606, -5.278564329441106651, 14.94126095370959462 ) ) ;
#1203=DIRECTION ( 'NONE',  ( -1.000000000000000000, -0.000000000000000000, -0.000000000000000000 ) ) ;
#1204=CARTESIAN_POINT ( 'NONE',  ( 2.789999999999999147, 13.40591150984226587, 7.739906618939754956 ) ) ;
#1205=ORIENTED_EDGE ( 'NONE', *, *, #12615, .F. ) ;
#1212=AXIS2_PLACEMENT_3D ( 'NONE', #1541, #6456, #606 ) ;
#1213=ORIENTED_EDGE ( 'NONE', *, *, #1383, .T. ) ;
#1216=ORIENTED_EDGE ( 'NONE', *, *, #6764, .F. ) ;
#1220=CARTESIAN_POINT ( 'NONE',  ( 0.008751532932800723183, 13.40591150984233870, -5.214906618939568084 ) ) ;
#1222=CARTESIAN_POINT ( 'NONE',  ( 0.02531912748464718033, -14.46287784598619020, 2.311161484776505404 ) ) ;
#1224=DIRECTION ( 'NONE',  ( -1.000000000000000000, -0.000000000000000000, -0.000000000000000000 ) ) ;
#1228=ORIENTED_EDGE ( 'NONE', *, *, #113, .T. ) ;
#1231=ORIENTED_EDGE ( 'NONE', *, *, #5249, .F. ) ;
#1234=VERTEX_POINT ( 'NONE', #9858 ) ;
#1235=VECTOR ( 'NONE', #28, 1000.000000000000000 ) ;
#1237=DIRECTION ( 'NONE',  ( 0.000000000000000000, 0.000000000000000000, 1.000000000000000000 ) ) ;
#1239=DIRECTION ( 'NONE',  ( 0.000000000000000000, 0.000000000000000000, 1.000000000000000000 ) ) ;
#1241=ORIENTED_EDGE ( 'NONE', *, *, #12909, .F. ) ;
#1248=ORIENTED_EDGE ( 'NONE', *, *, #12434, .T. ) ;
#1249=VERTEX_POINT ( 'NONE', #12389 ) ;
#1251=ORIENTED_EDGE ( 'NONE', *, *, #5443, .T. ) ;
#1252=DIRECTION ( 'NONE',  ( 0.000000000000000000, 0.000000000000000000, 1.000000000000000000 ) ) ;
#1257=ORIENTED_EDGE ( 'NONE', *, *, #3095, .T. ) ;
#1260=CARTESIAN_POINT ( 'NONE',  ( 2.789999999999999147, -12.98979500319697955, 5.249430348645709010 ) ) ;
#1261=ORIENTED_EDGE ( 'NONE', *, *, #10893, .T. ) ;
#1263=LINE ( 'NONE', #4589, #12939 ) ;
#1264=CARTESIAN_POINT ( 'NONE',  ( 0.000000000000000000, -1.948757464274081030, -13.87420763704363580 ) ) ;
#1265=DIRECTION ( 'NONE',  ( 0.000000000000000000, 0.000000000000000000, 1.000000000000000000 ) ) ;
#1267=DIRECTION ( 'NONE',  ( 0.000000000000000000, 3.435095992033281961E-15, -1.000000000000000000 ) ) ;
#1269=EDGE_CURVE ( 'NONE', #7725, #1234, #4254, .T. ) ;
#1274=CYLINDRICAL_SURFACE ( 'NONE', #4844, 8.399999999999998579 ) ;
#1277=EDGE_CURVE ( 'NONE', #799, #3527, #1714, .T. ) ;
#1279=FACE_OUTER_BOUND ( 'NONE', #7657, .T. ) ;
#1282=CARTESIAN_POINT ( 'NONE',  ( 2.782650494170373356, 13.44926448535263042, 5.204557061642334226 ) ) ;
#1286=VECTOR ( 'NONE', #5600, 1000.000000000000000 ) ;
#1298=ORIENTED_EDGE ( 'NONE', *, *, #14707, .F. ) ;
#1303=CARTESIAN_POINT ( 'NONE',  ( 1.749999999999999778, -12.55714665599977842, -12.83329210556845190 ) ) ;
#1306=CARTESIAN_POINT ( 'NONE',  ( 2.764680872515351773, 11.36963888406687317, 9.232963481057801403 ) ) ;
#1308=ORIENTED_EDGE ( 'NONE', *, *, #12340, .F. ) ;
#1316=VERTEX_POINT ( 'NONE', #12473 ) ;
#1317=ORIENTED_EDGE ( 'NONE', *, *, #8230, .T. ) ;
#1323=AXIS2_PLACEMENT_3D ( 'NONE', #1066, #6909, #2148 ) ;
#1330=CARTESIAN_POINT ( 'NONE',  ( 0.02531912748631555063, 2.311161484776756758, -14.46287784598614756 ) ) ;
#1333=EDGE_LOOP ( 'NONE', ( #5720, #12557, #14675, #8271, #7245, #5481, #849 ) ) ;
#1340=CARTESIAN_POINT ( 'NONE',  ( 2.789999999999999147, 13.87420763704361093, 1.948757464274220697 ) ) ;
#1347=LINE ( 'NONE', #10731, #35 ) ;
#1348=AXIS2_PLACEMENT_3D ( 'NONE', #11884, #8204, #12885 ) ;
#1351=CARTESIAN_POINT ( 'NONE',  ( -10.00000000000000000, 0.000000000000000000, 0.000000000000000000 ) ) ;
#1368=CYLINDRICAL_SURFACE ( 'NONE', #5612, 2.524999999999999467 ) ;
#1376=AXIS2_PLACEMENT_3D ( 'NONE', #7353, #6187, #9640 ) ;
#1377=ORIENTED_EDGE ( 'NONE', *, *, #5249, .T. ) ;
#1379=B_SPLINE_CURVE_WITH_KNOTS ( 'NONE', 3,
 ( #3174, #6631, #853, #13696, #10459, #10232, #7861, #11529 ),
 .UNSPECIFIED., .F., .F.,
 ( 4, 2, 2, 4 ),
 ( 2.445728210258510103E-07, 0.001895260649874686140, 0.002842768688401514036, 0.003790276726928342148 ),
 .UNSPECIFIED. ) ;
#1383=EDGE_CURVE ( 'NONE', #7996, #7166, #13791, .T. ) ;
#1387=CIRCLE ( 'NONE', #5569, 2.524999999999999023 ) ;
#1397=CARTESIAN_POINT ( 'NONE',  ( 2.789999999999999147, 0.000000000000000000, 0.000000000000000000 ) ) ;
#1398=CARTESIAN_POINT ( 'NONE',  ( 0.02531912748464631296, -13.68080036884344963, -5.229914364928496262 ) ) ;
#1400=VERTEX_POINT ( 'NONE', #4413 ) ;
#1402=VECTOR ( 'NONE', #4636, 1000.000000000000000 ) ;
#1406=B_SPLINE_CURVE_WITH_KNOTS ( 'NONE', 3,
 ( #14050, #3453, #8069, #14211 ),
 .UNSPECIFIED., .F., .F.,
 ( 4, 4 ),
 ( 0.005123713096549377226, 0.005814346476695811915 ),
 .UNSPECIFIED. ) ;
#1408=ORIENTED_EDGE ( 'NONE', *, *, #1194, .F. ) ;
#1409=CARTESIAN_POINT ( 'NONE',  ( 0.000000000000000000, 1.948757464274368578, -13.87420763704359494 ) ) ;
#1410=CARTESIAN_POINT ( 'NONE',  ( 2.508169649284527125, -15.84037596932105707, -3.072260951847695765 ) ) ;
#1416=LINE ( 'NONE', #9630, #267 ) ;
#1420=VERTEX_POINT ( 'NONE', #4329 ) ;
#1421=DIRECTION ( 'NONE',  ( 1.000000000000000000, 0.000000000000000000, 0.000000000000000000 ) ) ;
#1422=ORIENTED_EDGE ( 'NONE', *, *, #790, .T. ) ;
#1432=VERTEX_POINT ( 'NONE', #8007 ) ;
#1433=CARTESIAN_POINT ( 'NONE',  ( 1.885839510111769979, -4.928563447326406610, 17.01651022436361771 ) ) ;
#1438=ORIENTED_EDGE ( 'NONE', *, *, #5807, .F. ) ;
#1439=VERTEX_POINT ( 'NONE', #5711 ) ;
#1448=CARTESIAN_POINT ( 'NONE',  ( 1.749999999999999778, 4.835383649608716361, -17.29145405592683815 ) ) ;
#1449=ORIENTED_EDGE ( 'NONE', *, *, #14328, .F. ) ;
#1450=CARTESIAN_POINT ( 'NONE',  ( 1.039999999999997593, 0.000000000000000000, 0.000000000000000000 ) ) ;
#1451=CARTESIAN_POINT ( 'NONE',  ( 2.790000000000060876, 11.12234047011190263, 8.842064619038561446 ) ) ;
#1455=AXIS2_PLACEMENT_3D ( 'NONE', #11857, #7631, #8405 ) ;
#1460=CARTESIAN_POINT ( 'NONE',  ( 1.749999999999999778, 17.39253030560841395, -4.458161950358560333 ) ) ;
#1483=CARTESIAN_POINT ( 'NONE',  ( 0.000000000000000000, 0.000000000000000000, 0.000000000000000000 ) ) ;
#1484=EDGE_CURVE ( 'NONE', #10057, #393, #5096, .T. ) ;
#1495=CARTESIAN_POINT ( 'NONE',  ( 0.1920562174424405855, 12.05486625177571547, 10.28947301956286431 ) ) ;
#1503=EDGE_CURVE ( 'NONE', #7572, #3527, #300, .T. ) ;
#1508=CARTESIAN_POINT ( 'NONE',  ( 2.789999999999999147, 14.19996452731195546, -4.595504208219880482 ) ) ;
#1509=ORIENTED_EDGE ( 'NONE', *, *, #4495, .T. ) ;
#1516=CARTESIAN_POINT ( 'NONE',  ( 1.749999999999999778, 4.458161950358745074, -17.39253030560836777 ) ) ;
#1525=LINE ( 'NONE', #9830, #6536 ) ;
#1541=CARTESIAN_POINT ( 'NONE',  ( 1.039999999999997593, 0.000000000000000000, 0.000000000000000000 ) ) ;
#1544=ORIENTED_EDGE ( 'NONE', *, *, #12438, .F. ) ;
#1545=DIRECTION ( 'NONE',  ( 0.000000000000000000, 0.000000000000000000, 1.000000000000000000 ) ) ;
#1549=DIRECTION ( 'NONE',  ( -1.000000000000000000, -0.000000000000000000, -0.000000000000000000 ) ) ;
#1553=ORIENTED_EDGE ( 'NONE', *, *, #8444, .F. ) ;
#1564=DIRECTION ( 'NONE',  ( -1.000000000000000000, -0.000000000000000000, 0.000000000000000000 ) ) ;
#1579=DIRECTION ( 'NONE',  ( 0.000000000000000000, 0.000000000000000000, -1.000000000000000000 ) ) ;
#1593=B_SPLINE_CURVE_WITH_KNOTS ( 'NONE', 3,
 ( #11439, #14838, #12594, #3081 ),
 .UNSPECIFIED., .F., .F.,
 ( 4, 4 ),
 ( 2.451234579310872104E-07, 0.0006917187676826492410 ),
 .UNSPECIFIED. ) ;
#1594=CARTESIAN_POINT ( 'NONE',  ( 0.000000000000000000, -5.249430348645662825, -12.98979500319700264 ) ) ;
#1597=CARTESIAN_POINT ( 'NONE',  ( 2.440610831926789182, 15.53033051714692014, 5.240368680323600259 ) ) ;
#1614=ORIENTED_EDGE ( 'NONE', *, *, #8614, .F. ) ;
#1623=CARTESIAN_POINT ( 'NONE',  ( 1.749999999999999778, 12.55714665599987079, 12.83329210556836308 ) ) ;
#1626=CIRCLE ( 'NONE', #5563, 17.95481323787947403 ) ;
#1632=VERTEX_POINT ( 'NONE', #10996 ) ;
#1639=CARTESIAN_POINT ( 'NONE',  ( 2.789999999999999147, -5.404747904883309660E-14, 15.47981323787947794 ) ) ;
#1640=VECTOR ( 'NONE', #1054, 1000.000000000000000 ) ;
#1654=EDGE_CURVE ( 'NONE', #9529, #3623, #15149, .T. ) ;
#1660=CARTESIAN_POINT ( 'NONE',  ( 2.337784068222785283, -5.191253194756122902, 15.84984805378629424 ) ) ;
#1662=AXIS2_PLACEMENT_3D ( 'NONE', #8352, #2747, #500 ) ;
#1670=EDGE_LOOP ( 'NONE', ( #5556, #3754, #10771, #4263 ) ) ;
#1673=CARTESIAN_POINT ( 'NONE',  ( 2.789999999999999147, -7.739906618939614624, -13.40591150984234581 ) ) ;
#1674=AXIS2_PLACEMENT_3D ( 'NONE', #967, #4359, #11491 ) ;
#1677=FACE_OUTER_BOUND ( 'NONE', #7827, .T. ) ;
#1684=CARTESIAN_POINT ( 'NONE',  ( 2.764680872513933796, 5.229914364928542447, -13.68080036884343009 ) ) ;
#1688=CIRCLE ( 'NONE', #8786, 2.524999999999999023 ) ;
#1689=TOROIDAL_SURFACE ( 'NONE', #9051, 14.01039946648073986, 8.000000000000000000 ) ;
#1710=CARTESIAN_POINT ( 'NONE',  ( 0.02531912748464674665, 11.36963888406700285, -9.232963481057645083 ) ) ;
#1713=EDGE_LOOP ( 'NONE', ( #6464, #13973, #12040, #4774 ) ) ;
#1714=B_SPLINE_CURVE_WITH_KNOTS ( 'NONE', 3,
 ( #5116, #2945, #627, #3951 ),
 .UNSPECIFIED., .F., .F.,
 ( 4, 4 ),
 ( 0.002880534149780423873, 0.003796793755617398208 ),
 .UNSPECIFIED. ) ;
#1716=ORIENTED_EDGE ( 'NONE', *, *, #6838, .T. ) ;
#1718=DIRECTION ( 'NONE',  ( 0.000000000000000000, 0.000000000000000000, 1.000000000000000000 ) ) ;
#1720=DIRECTION ( 'NONE',  ( -1.000000000000000000, -0.000000000000000000, 0.000000000000000000 ) ) ;
#1723=CARTESIAN_POINT ( 'NONE',  ( 0.5431870686475167576, 12.54666350726139790, -11.42270873787279761 ) ) ;
#1731=CARTESIAN_POINT ( 'NONE',  ( 8.000000000000000000, 0.000000000000000000, 0.000000000000000000 ) ) ;
#1733=LINE ( 'NONE', #5366, #10983 ) ;
#1736=CARTESIAN_POINT ( 'NONE',  ( 2.597943565934061727, -5.295083827234814855, 14.93837896275547905 ) ) ;
#1738=CYLINDRICAL_SURFACE ( 'NONE', #12242, 8.400000000000000355 ) ;
#1739=CARTESIAN_POINT ( 'NONE',  ( 1.039999999999996483, 17.39253030560841395, 4.458161950358563885 ) ) ;
#1745=CARTESIAN_POINT ( 'NONE',  ( 50.00050000000000239, 0.000000000000000000, 0.000000000000000000 ) ) ;
#1750=CARTESIAN_POINT ( 'NONE',  ( 1.039999999999997593, 0.000000000000000000, 0.000000000000000000 ) ) ;
#1751=ADVANCED_FACE ( 'NONE', ( #13452 ), #4577, .T. ) ;
#1756=CARTESIAN_POINT ( 'NONE',  ( 2.777260912398869852, 13.49730943211508816, -5.214906618940189809 ) ) ;
#1759=DIRECTION ( 'NONE',  ( 0.000000000000000000, 0.000000000000000000, 1.000000000000000000 ) ) ;
#1764=CARTESIAN_POINT ( 'NONE',  ( 2.764680872515352661, 5.229914364928351489, 13.68080036884350292 ) ) ;
#1768=EDGE_CURVE ( 'NONE', #12657, #7299, #13123, .T. ) ;
#1772=VERTEX_POINT ( 'NONE', #5624 ) ;
#1775=SURFACE_STYLE_USAGE ( .BOTH. , #381 ) ;
#1780=ADVANCED_FACE ( 'NONE', ( #844 ), #2361, .T. ) ;
#1793=DIRECTION ( 'NONE',  ( -1.000000000000000000, -0.000000000000000000, -0.000000000000000000 ) ) ;
#1795=EDGE_LOOP ( 'NONE', ( #14098, #13831, #14406, #12541, #7881, #1799, #7159, #1308 ) ) ;
#1796=CARTESIAN_POINT ( 'NONE',  ( 0.07473581742173279752, 14.31752701692944285, -5.299647274066949798 ) ) ;
#1797=CARTESIAN_POINT ( 'NONE',  ( 0.007327513813773455648, 13.44898112152234937, 5.204526028255736847 ) ) ;
#1799=ORIENTED_EDGE ( 'NONE', *, *, #7638, .T. ) ;
#1804=CARTESIAN_POINT ( 'NONE',  ( 2.790000000000009361, -2.096460570596073936, -14.05347802000171065 ) ) ;
#1806=CARTESIAN_POINT ( 'NONE',  ( -5.209999999999999964, 0.000000000000000000, 0.000000000000000000 ) ) ;
#1814=CARTESIAN_POINT ( 'NONE',  ( 0.007327532539344137376, 2.217238903388563109, 14.24942254254690255 ) ) ;
#1825=CARTESIAN_POINT ( 'NONE',  ( 1.749999999999999778, 17.29145405592695539, -4.835383649608290924 ) ) ;
#1826=VERTEX_POINT ( 'NONE', #3304 ) ;
#1827=DIRECTION ( 'NONE',  ( 0.000000000000000000, 0.000000000000000000, 1.000000000000000000 ) ) ;
#1842=CARTESIAN_POINT ( 'NONE',  ( 0.000000000000000000, -13.40591150984221080, -7.739906618939849103 ) ) ;
#1855=( NAMED_UNIT ( * ) SI_UNIT ( $, .STERADIAN. ) SOLID_ANGLE_UNIT ( ) );
#1857=EDGE_CURVE ( 'NONE', #3154, #6372, #5972, .T. ) ;
#1866=VECTOR ( 'NONE', #7703, 1000.000000000000000 ) ;
#1871=CARTESIAN_POINT ( 'NONE',  ( 0.4286645550874384480, 15.76776810790841310, 5.200734291367693274 ) ) ;
#1878=LINE ( 'NONE', #14642, #10434 ) ;
#1880=ORIENTED_EDGE ( 'NONE', *, *, #8495, .T. ) ;
#1881=DIRECTION ( 'NONE',  ( 0.000000000000000000, 0.000000000000000000, 1.000000000000000000 ) ) ;
#1888=AXIS2_PLACEMENT_3D ( 'NONE', #2323, #10170, #13712 ) ;
#1893=CIRCLE ( 'NONE', #10480, 17.95481323787947758 ) ;
#1894=VERTEX_POINT ( 'NONE', #8991 ) ;
#1901=DIRECTION ( 'NONE',  ( 0.000000000000000000, 0.000000000000000000, 1.000000000000000000 ) ) ;
#1903=PRODUCT_CONTEXT ( 'NONE', #13910, 'mechanical' ) ;
#1917=DIRECTION ( 'NONE',  ( 0.000000000000000000, 0.000000000000000000, 1.000000000000000000 ) ) ;
#1922=VERTEX_POINT ( 'NONE', #10671 ) ;
#1924=DIRECTION ( 'NONE',  ( -1.000000000000000000, -0.000000000000000000, -0.000000000000000000 ) ) ;
#1932=VERTEX_POINT ( 'NONE', #2604 ) ;
#1933=CARTESIAN_POINT ( 'NONE',  ( 8.000000000000000000, 0.000000000000000000, 0.000000000000000000 ) ) ;
#1937=ADVANCED_FACE ( 'NONE', ( #14133 ), #13407, .T. ) ;
#1952=CARTESIAN_POINT ( 'NONE',  ( 2.789999999999999147, 7.739906618939895289, -13.40591150984218416 ) ) ;
#1958=CARTESIAN_POINT ( 'NONE',  ( 0.02531912748605881155, 13.68080036884355621, -5.229914364928207604 ) ) ;
#1961=ORIENTED_EDGE ( 'NONE', *, *, #14379, .T. ) ;
#1968=ADVANCED_FACE ( 'NONE', ( #14053 ), #6050, .T. ) ;
#1970=DIRECTION ( 'NONE',  ( -1.000000000000000000, 0.000000000000000000, -0.000000000000000000 ) ) ;
#1985=CARTESIAN_POINT ( 'NONE',  ( 0.07473575470096431583, -9.749517823374088010, 11.74839219818084324 ) ) ;
#1986=EDGE_CURVE ( 'NONE', #9176, #13761, #14232, .T. ) ;
#1988=EDGE_LOOP ( 'NONE', ( #3045, #4241, #1408, #4625 ) ) ;
#1989=FACE_OUTER_BOUND ( 'NONE', #55, .T. ) ;
#1996=ORIENTED_EDGE ( 'NONE', *, *, #13788, .F. ) ;
#1999=CARTESIAN_POINT ( 'NONE',  ( 2.790000000000060876, -5.211197193340600720, -13.21862218141521339 ) ) ;
#2000=ORIENTED_EDGE ( 'NONE', *, *, #3343, .T. ) ;
#2002=FACE_OUTER_BOUND ( 'NONE', #150, .T. ) ;
#2004=DIRECTION ( 'NONE',  ( 0.000000000000000000, 0.000000000000000000, 1.000000000000000000 ) ) ;
#2005=ORIENTED_EDGE ( 'NONE', *, *, #11028, .F. ) ;
#2013=CARTESIAN_POINT ( 'NONE',  ( 1.039999999999997593, 0.000000000000000000, 0.000000000000000000 ) ) ;
#2021=AXIS2_PLACEMENT_3D ( 'NONE', #8124, #6895, #4908 ) ;
#2023=ORIENTED_EDGE ( 'NONE', *, *, #1183, .F. ) ;
#2031=EDGE_LOOP ( 'NONE', ( #7108, #9185, #13828, #4457 ) ) ;
#2032=EDGE_CURVE ( 'NONE', #5828, #10832, #1525, .T. ) ;
#2043=VERTEX_POINT ( 'NONE', #1684 ) ;
#2055=CARTESIAN_POINT ( 'NONE',  ( 2.764680872513935128, -5.229914364928447412, 13.68080036884346917 ) ) ;
#2056=ADVANCED_FACE ( 'NONE', ( #13435 ), #8595, .T. ) ;
#2061=DIRECTION ( 'NONE',  ( -1.000000000000000000, 0.000000000000000000, -0.000000000000000000 ) ) ;
#2073=AXIS2_PLACEMENT_3D ( 'NONE', #7314, #294, #1239 ) ;
#2074=ORIENTED_EDGE ( 'NONE', *, *, #9768, .F. ) ;
#2075=CARTESIAN_POINT ( 'NONE',  ( 1.749999999999999778, 17.39253030560841395, 4.458161950358562109 ) ) ;
#2077=LINE ( 'NONE', #13912, #5028 ) ;
#2085=VECTOR ( 'NONE', #3110, 1000.000000000000000 ) ;
#2093=VECTOR ( 'NONE', #10847, 1000.000000000000000 ) ;
#2096=DIRECTION ( 'NONE',  ( 0.000000000000000000, 0.000000000000000000, 1.000000000000000000 ) ) ;
#2097=CARTESIAN_POINT ( 'NONE',  ( 0.000000000000000000, -12.98979500319698488, 5.249430348645709010 ) ) ;
#2104=B_SPLINE_CURVE_WITH_KNOTS ( 'NONE', 3,
 ( #15134, #8562, #14496, #5751, #8129, #7053, #6972, #7419 ),
 .UNSPECIFIED., .F., .F.,
 ( 4, 2, 2, 4 ),
 ( 1.984117563342666817E-07, 0.001895214258086351218, 0.002842722181251362227, 0.003790230104416373452 ),
 .UNSPECIFIED. ) ;
#2106=CARTESIAN_POINT ( 'NONE',  ( 2.782650442329440921, -11.23191127083869567, 9.045126717605739941 ) ) ;
#2119=DIRECTION ( 'NONE',  ( 0.000000000000000000, 0.000000000000000000, 1.000000000000000000 ) ) ;
#2129=EDGE_CURVE ( 'NONE', #228, #7999, #1387, .T. ) ;
#2130=ORIENTED_EDGE ( 'NONE', *, *, #840, .F. ) ;
#2131=CARTESIAN_POINT ( 'NONE',  ( 2.697960337741387882, 2.583706482362242873, -15.03709480088669359 ) ) ;
#2139=ORIENTED_EDGE ( 'NONE', *, *, #5417, .T. ) ;
#2144=DIRECTION ( 'NONE',  ( 0.000000000000000000, 0.000000000000000000, 1.000000000000000000 ) ) ;
#2146=AXIS2_PLACEMENT_3D ( 'NONE', #12759, #9157, #2169 ) ;
#2147=CARTESIAN_POINT ( 'NONE',  ( 2.597943646031691145, -15.58455734132168935, 2.883512197588957271 ) ) ;
#2148=DIRECTION ( 'NONE',  ( 0.000000000000000000, 0.000000000000000000, 1.000000000000000000 ) ) ;
#2157=CARTESIAN_POINT ( 'NONE',  ( 2.582362678678089551, 15.57879356040263197, 2.899259574942802065 ) ) ;
#2162=EDGE_LOOP ( 'NONE', ( #6708, #1880, #6992, #3959 ) ) ;
#2165=ORIENTED_EDGE ( 'NONE', *, *, #6171, .T. ) ;
#2169=DIRECTION ( 'NONE',  ( 0.000000000000000000, 0.000000000000000000, 1.000000000000000000 ) ) ;
#2176=CARTESIAN_POINT ( 'NONE',  ( 1.394999999999999574, 4.458161950358503489, 17.39253030560843172 ) ) ;
#2177=CARTESIAN_POINT ( 'NONE',  ( 0.5431871198829162362, 16.57708379306436441, -3.619024283482057847 ) ) ;
#2181=ORIENTED_EDGE ( 'NONE', *, *, #12438, .T. ) ;
#2184=ORIENTED_EDGE ( 'NONE', *, *, #10571, .F. ) ;
#2189=DIRECTION ( 'NONE',  ( 0.000000000000000000, -0.8660254037844397068, 0.4999999999999980571 ) ) ;
#2201=CARTESIAN_POINT ( 'NONE',  ( 1.039999999999998259, -12.83329210556822986, -12.55714665600000757 ) ) ;
#2202=AXIS2_PLACEMENT_3D ( 'NONE', #692, #12593, #5402 ) ;
#2218=CARTESIAN_POINT ( 'NONE',  ( 1.394999999999998685, 12.83329210556849276, -12.55714665599973756 ) ) ;
#2221=CARTESIAN_POINT ( 'NONE',  ( 1.039999999999997149, 17.39253030560841751, -4.458161950358562997 ) ) ;
#2246=VERTEX_POINT ( 'NONE', #6518 ) ;
#2251=ORIENTED_EDGE ( 'NONE', *, *, #3001, .F. ) ;
#2261=CARTESIAN_POINT ( 'NONE',  ( 2.764680872515354437, 13.68080036884355621, -5.229914364928207604 ) ) ;
#2262=CARTESIAN_POINT ( 'NONE',  ( 2.790000000000008029, -11.12243880662619233, 8.842327429719055942 ) ) ;
#2264=FACE_OUTER_BOUND ( 'NONE', #3407, .T. ) ;
#2277=CARTESIAN_POINT ( 'NONE',  ( 0.000000000000000000, 13.87420763704361448, -1.948757464274226470 ) ) ;
#2285=DIRECTION ( 'NONE',  ( 0.000000000000000000, 0.000000000000000000, 1.000000000000000000 ) ) ;
#2300=EDGE_LOOP ( 'NONE', ( #12748, #556, #6236, #6495 ) ) ;
#2307=( NAMED_UNIT ( * ) SI_UNIT ( $, .STERADIAN. ) SOLID_ANGLE_UNIT ( ) );
#2309=CARTESIAN_POINT ( 'NONE',  ( 0.02531912748464674665, 5.229914364928542447, -13.68080036884343009 ) ) ;
#2311=AXIS2_PLACEMENT_3D ( 'NONE', #5729, #1186, #3418 ) ;
#2312=CARTESIAN_POINT ( 'NONE',  ( 0.5431871198829543168, -3.619024283481952597, -16.57708379306448165 ) ) ;
#2323=CARTESIAN_POINT ( 'NONE',  ( 1.749999999999999778, 0.000000000000000000, 0.000000000000000000 ) ) ;
#2327=DIRECTION ( 'NONE',  ( 0.000000000000000000, 0.000000000000000000, 1.000000000000000000 ) ) ;
#2331=AXIS2_PLACEMENT_3D ( 'NONE', #8, #10391, #11614 ) ;
#2334=B_SPLINE_CURVE_WITH_KNOTS ( 'NONE', 3,
 ( #8832, #451, #5092, #13526 ),
 .UNSPECIFIED., .F., .F.,
 ( 4, 4 ),
 ( 2.451234579287542699E-07, 0.0006917187676826530357 ),
 .UNSPECIFIED. ) ;
#2344=AXIS2_PLACEMENT_3D ( 'NONE', #1397, #7090, #2479 ) ;
#2346=CARTESIAN_POINT ( 'NONE',  ( 0.7686372590627849055, -5.021526291670431519, 16.74220655292935334 ) ) ;
#2348=CARTESIAN_POINT ( 'NONE',  ( 2.246812850058911071, 5.154374911958910843, 16.16568790143443479 ) ) ;
#2353=VECTOR ( 'NONE', #6220, 1000.000000000000000 ) ;
#2361=TOROIDAL_SURFACE ( 'NONE', #647, 14.01039946648074341, 8.000000000000000000 ) ;
#2364=CARTESIAN_POINT ( 'NONE',  ( 2.010451923687323728, 12.70439593876677620, -11.98750039041481408 ) ) ;
#2367=MECHANICAL_DESIGN_GEOMETRIC_PRESENTATION_REPRESENTATION('',(#1143),#8251);
#2368=LINE ( 'NONE', #7203, #7795 ) ;
#2369=DIRECTION ( 'NONE',  ( 0.000000000000000000, 0.000000000000000000, 1.000000000000000000 ) ) ;
#2371=CARTESIAN_POINT ( 'NONE',  ( 2.764680872513682885, -14.46287784598619020, 2.311161484776505404 ) ) ;
#2373=EDGE_LOOP ( 'NONE', ( #4963, #5156, #10411, #2444, #7197, #1961, #1248, #9854 ) ) ;
#2374=AXIS2_PLACEMENT_3D ( 'NONE', #1351, #3662, #3731 ) ;
#2383=VERTEX_POINT ( 'NONE', #14268 ) ;
#2386=CYLINDRICAL_SURFACE ( 'NONE', #905, 8.400000000000000355 ) ;
#2387=CARTESIAN_POINT ( 'NONE',  ( 0.02531912748679390063, 9.232963481057920418, -11.36963888406677725 ) ) ;
#2397=ORIENTED_EDGE ( 'NONE', *, *, #13935, .F. ) ;
#2399=CARTESIAN_POINT ( 'NONE',  ( 2.789999999999999147, 0.000000000000000000, 0.000000000000000000 ) ) ;
#2412=CARTESIAN_POINT ( 'NONE',  ( 2.764680872513682441, -2.311161484776455222, -14.46287784598619908 ) ) ;
#2417=EDGE_CURVE ( 'NONE', #6870, #10268, #1347, .T. ) ;
#2420=VECTOR ( 'NONE', #10730, 1000.000000000000000 ) ;
#2424=EDGE_CURVE ( 'NONE', #7858, #10809, #8639, .T. ) ;
#2425=ORIENTED_EDGE ( 'NONE', *, *, #14370, .F. ) ;
#2426=CARTESIAN_POINT ( 'NONE',  ( 0.09203968221122213467, -5.280991956247218511, 14.31435947614540538 ) ) ;
#2428=ADVANCED_FACE ( 'NONE', ( #9579 ), #8053, .T. ) ;
#2435=CARTESIAN_POINT ( 'NONE',  ( 2.597943646031689813, 2.883512197589014558, 15.58455734132167869 ) ) ;
#2444=ORIENTED_EDGE ( 'NONE', *, *, #6440, .T. ) ;
#2445=EDGE_CURVE ( 'NONE', #960, #1432, #3722, .T. ) ;
#2447=ORIENTED_EDGE ( 'NONE', *, *, #6573, .T. ) ;
#2448=CARTESIAN_POINT ( 'NONE',  ( 0.04999670013151677472, 9.490919315500136122, 11.55877992729668691 ) ) ;
#2450=ADVANCED_FACE ( 'NONE', ( #493 ), #14507, .F. ) ;
#2451=DIRECTION ( 'NONE',  ( -1.000000000000000000, -0.000000000000000000, 0.000000000000000000 ) ) ;
#2455=VERTEX_POINT ( 'NONE', #13412 ) ;
#2461=CARTESIAN_POINT ( 'NONE',  ( 0.000000000000000000, 0.000000000000000000, 0.000000000000000000 ) ) ;
#2468=ORIENTED_EDGE ( 'NONE', *, *, #14073, .T. ) ;
#2472=CARTESIAN_POINT ( 'NONE',  ( 2.697960337741385217, -2.583706482362138512, 15.03709480088670603 ) ) ;
#2473=CARTESIAN_POINT ( 'NONE',  ( 0.7795480803411065640, -4.029281904976750539, 16.99607982911240001 ) ) ;
#2479=DIRECTION ( 'NONE',  ( 0.000000000000000000, 0.000000000000000000, 1.000000000000000000 ) ) ;
#2495=ORIENTED_EDGE ( 'NONE', *, *, #5362, .T. ) ;
#2496=CARTESIAN_POINT ( 'NONE',  ( 0.9041604711286037599, -12.77651625388890544, -12.27244837507626585 ) ) ;
#2505=ORIENTED_EDGE ( 'NONE', *, *, #14754, .T. ) ;
#2509=FACE_OUTER_BOUND ( 'NONE', #1196, .T. ) ;
#2515=VERTEX_POINT ( 'NONE', #9810 ) ;
#2516=CARTESIAN_POINT ( 'NONE',  ( 2.337784053193427969, 12.42068120944096776, -11.13074453164190913 ) ) ;
#2518=CARTESIAN_POINT ( 'NONE',  ( 2.789999999999999147, 9.232963481057920418, -11.36963888406677725 ) ) ;
#2523=ORIENTED_EDGE ( 'NONE', *, *, #1156, .F. ) ;
#2525=DIRECTION ( 'NONE',  ( -1.000000000000000000, -0.000000000000000000, -0.000000000000000000 ) ) ;
#2531=EDGE_CURVE ( 'NONE', #10080, #212, #12324, .T. ) ;
#2533=ORIENTED_EDGE ( 'NONE', *, *, #14679, .F. ) ;
#2535=ORIENTED_EDGE ( 'NONE', *, *, #5195, .T. ) ;
#2540=CARTESIAN_POINT ( 'NONE',  ( 2.010451923687323283, -11.98750039041484783, -12.70439593876673001 ) ) ;
#2554=DIRECTION ( 'NONE',  ( 0.000000000000000000, 0.000000000000000000, 1.000000000000000000 ) ) ;
#2561=DIRECTION ( 'NONE',  ( 0.000000000000000000, 0.000000000000000000, 1.000000000000000000 ) ) ;
#2567=VERTEX_POINT ( 'NONE', #6123 ) ;
#2570=AXIS2_PLACEMENT_3D ( 'NONE', #3704, #11841, #2554 ) ;
#2572=CARTESIAN_POINT ( 'NONE',  ( 2.582362639458681386, 5.278564329441002734, 14.94126095370962837 ) ) ;
#2574=CARTESIAN_POINT ( 'NONE',  ( 2.789999999999999147, -13.40591150984231916, 7.739906618939660810 ) ) ;
#2581=CARTESIAN_POINT ( 'NONE',  ( 2.715264205769515105, -2.569134216958794070, -15.04916547791957271 ) ) ;
#2583=FACE_OUTER_BOUND ( 'NONE', #2300, .T. ) ;
#2596=CARTESIAN_POINT ( 'NONE',  ( 2.764680872513933796, 5.229914364928542447, -13.68080036884343009 ) ) ;
#2598=EDGE_CURVE ( 'NONE', #14375, #406, #8802, .T. ) ;
#2603=CARTESIAN_POINT ( 'NONE',  ( 2.789999999999999147, -7.739906618939614624, -13.40591150984234581 ) ) ;
#2604=CARTESIAN_POINT ( 'NONE',  ( 1.749999999999999778, 12.55714665599987079, 12.83329210556836308 ) ) ;
#2607=ORIENTED_EDGE ( 'NONE', *, *, #13060, .F. ) ;
#2614=CARTESIAN_POINT ( 'NONE',  ( 2.764680872515352661, -14.46287784598615644, -2.311161484776706576 ) ) ;
#2616=CARTESIAN_POINT ( 'NONE',  ( 0.000000000000000000, 0.000000000000000000, 4.000000000000000000 ) ) ;
#2617=CARTESIAN_POINT ( 'NONE',  ( 0.5537796532149699136, 16.55730827443880671, 3.624349476775253986 ) ) ;
#2618=CYLINDRICAL_SURFACE ( 'NONE', #2073, 17.95481323787947403 ) ;
#2623=CARTESIAN_POINT ( 'NONE',  ( 2.740003299868484898, 11.55877992729665316, 9.490919315500171649 ) ) ;
#2642=CARTESIAN_POINT ( 'NONE',  ( 0.000000000000000000, 0.000000000000000000, 0.000000000000000000 ) ) ;
#2643=CARTESIAN_POINT ( 'NONE',  ( 0.000000000000000000, -13.87420763704360382, -1.948757464274321949 ) ) ;
#2645=CARTESIAN_POINT ( 'NONE',  ( 2.789999999999999147, 7.739906618939895289, -13.40591150984218416 ) ) ;
#2647=TOROIDAL_SURFACE ( 'NONE', #9756, 14.01039946648074341, 8.000000000000000000 ) ;
#2653=ORIENTED_EDGE ( 'NONE', *, *, #7297, .T. ) ;
#2654=CARTESIAN_POINT ( 'NONE',  ( 0.9041604711286033158, 12.77651625388899248, 12.27244837507617881 ) ) ;
#2657=CARTESIAN_POINT ( 'NONE',  ( 2.764680872513208154, 9.232963481057765875, 11.36963888406690870 ) ) ;
#2665=B_SPLINE_CURVE_WITH_KNOTS ( 'NONE', 3,
 ( #1086, #7158, #2312, #4641, #14304, #7002, #11680, #10690 ),
 .UNSPECIFIED., .F., .F.,
 ( 4, 2, 2, 4 ),
 ( 4.663089412835749521E-07, 0.001898630173449115206, 0.002847712105703030603, 0.003796794037956946217 ),
 .UNSPECIFIED. ) ;
#2666=ORIENTED_EDGE ( 'NONE', *, *, #1183, .T. ) ;
#2671=ORIENTED_EDGE ( 'NONE', *, *, #11542, .F. ) ;
#2681=CARTESIAN_POINT ( 'NONE',  ( 2.789999999999999147, 12.98979500319694047, 5.249430348645800493 ) ) ;
#2693=CARTESIAN_POINT ( 'NONE',  ( 0.2076372544708476597, -12.04200105039477720, 10.30022894898801766 ) ) ;
#2694=DIRECTION ( 'NONE',  ( 0.000000000000000000, 0.000000000000000000, 1.000000000000000000 ) ) ;
#2695=ORIENTED_EDGE ( 'NONE', *, *, #14679, .T. ) ;
#2700=CARTESIAN_POINT ( 'NONE',  ( 2.246812880117042610, -3.619024283482186632, 16.57708379306443192 ) ) ;
#2702=DIRECTION ( 'NONE',  ( 0.000000000000000000, 0.000000000000000000, 1.000000000000000000 ) ) ;
#2725=DIRECTION ( 'NONE',  ( -1.000000000000000000, -0.000000000000000000, -0.000000000000000000 ) ) ;
#2727=CARTESIAN_POINT ( 'NONE',  ( 0.09203962824862134406, 11.73065272960076832, -9.756102650610117166 ) ) ;
#2729=CARTESIAN_POINT ( 'NONE',  ( 0.000000000000000000, -12.98979500319698488, 5.249430348645709010 ) ) ;
#2731=EDGE_LOOP ( 'NONE', ( #3627, #2505, #5199, #13701 ) ) ;
#2735=EDGE_CURVE ( 'NONE', #1249, #1439, #13083, .T. ) ;
#2738=ORIENTED_EDGE ( 'NONE', *, *, #6852, .F. ) ;
#2739=CARTESIAN_POINT ( 'NONE',  ( 1.749999999999999778, -4.835383649608602674, 17.29145405592687013 ) ) ;
#2747=DIRECTION ( 'NONE',  ( -1.000000000000000000, -0.000000000000000000, -0.000000000000000000 ) ) ;
#2751=CARTESIAN_POINT ( 'NONE',  ( 1.955869215373660985, 16.87476769693374123, 4.976600677180526233 ) ) ;
#2753=DIRECTION ( 'NONE',  ( -1.000000000000000000, -0.000000000000000000, -0.000000000000000000 ) ) ;
#2763=ORIENTED_EDGE ( 'NONE', *, *, #936, .F. ) ;
#2765=EDGE_LOOP ( 'NONE', ( #8581, #8099, #9477, #3972, #4007, #4237 ) ) ;
#2767=DIRECTION ( 'NONE',  ( -1.000000000000000000, -0.000000000000000000, -0.000000000000000000 ) ) ;
#2770=DIRECTION ( 'NONE',  ( -1.000000000000000000, -0.000000000000000000, -0.000000000000000000 ) ) ;
#2773=VERTEX_POINT ( 'NONE', #11331 ) ;
#2774=CARTESIAN_POINT ( 'NONE',  ( 0.000000000000000000, -11.04103753892277417, 8.624777288397769581 ) ) ;
#2775=ADVANCED_FACE ( 'NONE', ( #2264 ), #10128, .T. ) ;
#2778=ORIENTED_EDGE ( 'NONE', *, *, #3175, .T. ) ;
#2781=CARTESIAN_POINT ( 'NONE',  ( 2.789999999999999147, -14.59528211760000005, -3.120158876139185189 ) ) ;
#2792=DIRECTION ( 'NONE',  ( -1.000000000000000000, -0.000000000000000000, -0.000000000000000000 ) ) ;
#2795=ORIENTED_EDGE ( 'NONE', *, *, #11404, .F. ) ;
#2798=CARTESIAN_POINT ( 'NONE',  ( 2.789999999999999147, -14.59528211760004446, 3.120158876138978687 ) ) ;
#2815=VECTOR ( 'NONE', #7634, 1000.000000000000000 ) ;
#2821=DIRECTION ( 'NONE',  ( -1.000000000000000000, 0.000000000000000000, 0.000000000000000000 ) ) ;
#2828=ORIENTED_EDGE ( 'NONE', *, *, #8518, .F. ) ;
#2836=CARTESIAN_POINT ( 'NONE',  ( 2.764680872513688659, 2.311161484776556030, 14.46287784598618309 ) ) ;
#2838=ORIENTED_EDGE ( 'NONE', *, *, #5024, .F. ) ;
#2841=DIRECTION ( 'NONE',  ( -1.000000000000000000, -0.000000000000000000, -0.000000000000000000 ) ) ;
#2842=CARTESIAN_POINT ( 'NONE',  ( 0.4522159373304736607, -16.32199768300077380, -3.429166897524598134 ) ) ;
#2846=B_SPLINE_CURVE_WITH_KNOTS ( 'NONE', 3,
 ( #4313, #14926, #10304, #13763 ),
 .UNSPECIFIED., .F., .F.,
 ( 4, 4 ),
 ( 2.159563976582245544E-07, 0.0006916893629248793826 ),
 .UNSPECIFIED. ) ;
#2847=EDGE_CURVE ( 'NONE', #8589, #5623, #4685, .T. ) ;
#2850=B_SPLINE_CURVE_WITH_KNOTS ( 'NONE', 3,
 ( #12608, #5642, #12686, #11380 ),
 .UNSPECIFIED., .F., .F.,
 ( 4, 4 ),
 ( 0.005123695899043908056, 0.005814329666474866640 ),
 .UNSPECIFIED. ) ;
#2854=EDGE_LOOP ( 'NONE', ( #9779, #14271, #2653, #12124 ) ) ;
#2858=ORIENTED_EDGE ( 'NONE', *, *, #5653, .T. ) ;
#2862=AXIS2_PLACEMENT_3D ( 'NONE', #7345, #3955, #5268 ) ;
#2867=CARTESIAN_POINT ( 'NONE',  ( 1.749999999999999778, 12.83329210556849453, -12.55714665599973578 ) ) ;
#2873=CARTESIAN_POINT ( 'NONE',  ( 0.008751532932800723183, 13.40591150984233870, -5.214906618939568084 ) ) ;
#2875=CARTESIAN_POINT ( 'NONE',  ( 1.394999999999998685, 12.55714665600005375, -12.83329210556818722 ) ) ;
#2876=TOROIDAL_SURFACE ( 'NONE', #2146, 14.01039946648074341, 8.000000000000000000 ) ;
#2905=CARTESIAN_POINT ( 'NONE',  ( -5.209999999999999964, 0.000000000000000000, 0.000000000000000000 ) ) ;
#2907=DIRECTION ( 'NONE',  ( 0.000000000000000000, 0.000000000000000000, 1.000000000000000000 ) ) ;
#2911=CARTESIAN_POINT ( 'NONE',  ( 2.789999999999999147, -8.624777288397723396, -11.04103753892280615 ) ) ;
#2921=CARTESIAN_POINT ( 'NONE',  ( 2.789999999999999147, 1.621424371464993087E-13, -15.47981323787947794 ) ) ;
#2923=ORIENTED_EDGE ( 'NONE', *, *, #6352, .F. ) ;
#2925=CARTESIAN_POINT ( 'NONE',  ( 0.000000000000000000, -7.739906618939614624, -13.40591150984234581 ) ) ;
#2933=VECTOR ( 'NONE', #3430, 1000.000000000000000 ) ;
#2936=EDGE_LOOP ( 'NONE', ( #9229, #2778, #1228, #8215 ) ) ;
#2940=CARTESIAN_POINT ( 'NONE',  ( 2.790000000000010694, -14.05347802000170354, 2.096460570596122341 ) ) ;
#2945=CARTESIAN_POINT ( 'NONE',  ( 0.08915872821341043475, 14.29252738795465483, 5.279841123860395058 ) ) ;
#2948=FACE_OUTER_BOUND ( 'NONE', #10756, .T. ) ;
#2961=CARTESIAN_POINT ( 'NONE',  ( 2.782672435525938237, -9.044896821682277377, 11.23174270417326071 ) ) ;
#2968=ORIENTED_EDGE ( 'NONE', *, *, #14230, .F. ) ;
#2975=DIRECTION ( 'NONE',  ( 0.000000000000000000, 0.000000000000000000, 1.000000000000000000 ) ) ;
#2977=CARTESIAN_POINT ( 'NONE',  ( 0.02531912748679129854, -9.232963481057844035, 11.36963888406684298 ) ) ;
#2978=PLANE ( 'NONE',  #14489 ) ;
#2985=AXIS2_PLACEMENT_3D ( 'NONE', #7936, #1793, #6705 ) ;
#2993=CARTESIAN_POINT ( 'NONE',  ( 2.789999999999999147, 5.249430348645756084, 12.98979500319695823 ) ) ;
#3001=EDGE_CURVE ( 'NONE', #4926, #10057, #13355, .T. ) ;
#3002=ORIENTED_EDGE ( 'NONE', *, *, #6852, .T. ) ;
#3008=CIRCLE ( 'NONE', #11105, 14.01039946648073986 ) ;
#3014=LINE ( 'NONE', #14482, #6999 ) ;
#3018=B_SPLINE_CURVE_WITH_KNOTS ( 'NONE', 3,
 ( #15137, #7201, #41, #2516, #12878, #2364, #7056, #9426 ),
 .UNSPECIFIED., .F., .F.,
 ( 4, 2, 2, 4 ),
 ( 2.445728210258510103E-07, 0.001895260649874684405, 0.002842768688401516204, 0.003790276726928348220 ),
 .UNSPECIFIED. ) ;
#3026=CARTESIAN_POINT ( 'NONE',  ( 0.02531912748464587928, -5.229914364928447412, 13.68080036884346917 ) ) ;
#3027=CARTESIAN_POINT ( 'NONE',  ( 2.508169719062756986, -12.18203740414259606, -10.58084377126636078 ) ) ;
#3042=DIRECTION ( 'NONE',  ( -1.000000000000000000, -0.000000000000000000, 0.000000000000000000 ) ) ;
#3044=VERTEX_POINT ( 'NONE', #8916 ) ;
#3045=ORIENTED_EDGE ( 'NONE', *, *, #8959, .F. ) ;
#3054=DIRECTION ( 'NONE',  ( 1.000000000000000000, 0.000000000000000000, 0.000000000000000000 ) ) ;
#3056=AXIS2_PLACEMENT_3D ( 'NONE', #5225, #13347, #3748 ) ;
#3060=CARTESIAN_POINT ( 'NONE',  ( 2.781248467067199748, -13.40591150984217705, -5.214906618939849636 ) ) ;
#3069=VERTEX_POINT ( 'NONE', #13686 ) ;
#3070=ORIENTED_EDGE ( 'NONE', *, *, #7425, .T. ) ;
#3075=CARTESIAN_POINT ( 'NONE',  ( 2.790000000000009805, 2.096460570596172968, 14.05347802000169644 ) ) ;
#3078=VECTOR ( 'NONE', #8387, 1000.000000000000000 ) ;
#3080=DIRECTION ( 'NONE',  ( -1.000000000000000000, 0.000000000000000000, -0.000000000000000000 ) ) ;
#3081=CARTESIAN_POINT ( 'NONE',  ( 0.000000000000000000, -8.624777288397730501, -11.04103753892280615 ) ) ;
#3084=EDGE_CURVE ( 'NONE', #4197, #6222, #2846, .T. ) ;
#3095=EDGE_CURVE ( 'NONE', #13251, #13045, #2077, .T. ) ;
#3101=VERTEX_POINT ( 'NONE', #3238 ) ;
#3103=DIRECTION ( 'NONE',  ( -1.000000000000000000, 0.000000000000000000, 0.000000000000000000 ) ) ;
#3110=DIRECTION ( 'NONE',  ( -1.000000000000000000, 0.000000000000000000, 0.000000000000000000 ) ) ;
#3112=ORIENTED_EDGE ( 'NONE', *, *, #4796, .T. ) ;
#3126=ORIENTED_EDGE ( 'NONE', *, *, #5165, .F. ) ;
#3128=CARTESIAN_POINT ( 'NONE',  ( 0.5431871198829544278, 3.619024283482072946, 16.57708379306446034 ) ) ;
#3132=CARTESIAN_POINT ( 'NONE',  ( 0.02531912748464848137, 2.311161484776556030, 14.46287784598618309 ) ) ;
#3139=CARTESIAN_POINT ( 'NONE',  ( 1.749999999999999778, 17.29145405592695539, -4.835383649608290924 ) ) ;
#3140=CARTESIAN_POINT ( 'NONE',  ( 2.764680872515351329, 14.46287784598617421, -2.311161484776606212 ) ) ;
#3142=VERTEX_POINT ( 'NONE', #6918 ) ;
#3145=CARTESIAN_POINT ( 'NONE',  ( 2.764680872515351329, -11.36963888406680923, -9.232963481057881339 ) ) ;
#3154=VERTEX_POINT ( 'NONE', #13830 ) ;
#3159=LINE ( 'NONE', #3298, #8682 ) ;
#3169=ORIENTED_EDGE ( 'NONE', *, *, #12361, .T. ) ;
#3171=ORIENTED_EDGE ( 'NONE', *, *, #8319, .F. ) ;
#3174=CARTESIAN_POINT ( 'NONE',  ( 2.764680872513205934, -11.36963888406694068, 9.232963481057725019 ) ) ;
#3175=EDGE_CURVE ( 'NONE', #8536, #13456, #11595, .T. ) ;
#3177=CIRCLE ( 'NONE', #8312, 17.95481323787947758 ) ;
#3178=CIRCLE ( 'NONE', #7357, 2.524999999999999023 ) ;
#3186=EDGE_CURVE ( 'NONE', #1061, #9201, #4543, .T. ) ;
#3189=ORIENTED_EDGE ( 'NONE', *, *, #5076, .F. ) ;
#3199=CARTESIAN_POINT ( 'NONE',  ( 2.790000000000060876, -8.842064619038600526, 11.12234047011187421 ) ) ;
#3218=ORIENTED_EDGE ( 'NONE', *, *, #8150, .F. ) ;
#3219=DIRECTION ( 'NONE',  ( -1.000000000000000000, 0.000000000000000000, 0.000000000000000000 ) ) ;
#3225=ORIENTED_EDGE ( 'NONE', *, *, #5906, .F. ) ;
#3228=CYLINDRICAL_SURFACE ( 'NONE', #11719, 17.95481323787947403 ) ;
#3230=CARTESIAN_POINT ( 'NONE',  ( 2.789999999999999147, 1.948757464274366136, -13.87420763704359139 ) ) ;
#3236=B_SPLINE_CURVE_WITH_KNOTS ( 'NONE', 3,
 ( #9166, #6936, #2177, #13847, #8094, #15089, #4563, #9244 ),
 .UNSPECIFIED., .F., .F.,
 ( 4, 2, 2, 4 ),
 ( 4.663089413031289195E-07, 0.001898630173449298219, 0.002847712105703296016, 0.003796794037957293595 ),
 .UNSPECIFIED. ) ;
#3237=DIRECTION ( 'NONE',  ( 0.000000000000000000, 0.000000000000000000, 1.000000000000000000 ) ) ;
#3238=CARTESIAN_POINT ( 'NONE',  ( 0.000000000000000000, 4.898587196589412829E-16, -4.000000000000000000 ) ) ;
#3246=CARTESIAN_POINT ( 'NONE',  ( 2.740003281797977586, -5.264737421541426876, -13.99876742897264847 ) ) ;
#3270=ADVANCED_FACE ( 'NONE', ( #210 ), #8291, .T. ) ;
#3283=LINE ( 'NONE', #10126, #11495 ) ;
#3285=LINE ( 'NONE', #6675, #1640 ) ;
#3291=AXIS2_PLACEMENT_3D ( 'NONE', #6878, #11558, #15191 ) ;
#3298=CARTESIAN_POINT ( 'NONE',  ( 1.394999999999999574, 17.39253030560841751, 4.458161950358562109 ) ) ;
#3304=CARTESIAN_POINT ( 'NONE',  ( 2.789999999999999147, -7.739906618939614624, -10.88091150984234545 ) ) ;
#3309=ORIENTED_EDGE ( 'NONE', *, *, #8893, .F. ) ;
#3317=EDGE_CURVE ( 'NONE', #367, #12499, #9243, .T. ) ;
#3327=DIRECTION ( 'NONE',  ( -1.000000000000000000, -0.000000000000000000, -0.000000000000000000 ) ) ;
#3338=CARTESIAN_POINT ( 'NONE',  ( 2.550660015654387269, -15.07093484180036924, 5.269646308239033239 ) ) ;
#3343=EDGE_CURVE ( 'NONE', #12627, #6646, #13899, .T. ) ;
#3347=CARTESIAN_POINT ( 'NONE',  ( 0.7795480763126747537, -12.70439593876652218, -11.98750039041507343 ) ) ;
#3360=FACE_OUTER_BOUND ( 'NONE', #14931, .T. ) ;
#3367=ORIENTED_EDGE ( 'NONE', *, *, #1269, .F. ) ;
#3374=DIRECTION ( 'NONE',  ( -1.000000000000000000, -0.000000000000000000, -0.000000000000000000 ) ) ;
#3376=VERTEX_POINT ( 'NONE', #11054 ) ;
#3377=AXIS2_PLACEMENT_3D ( 'NONE', #9765, #2767, #5398 ) ;
#3380=DIRECTION ( 'NONE',  ( -1.000000000000000000, -0.000000000000000000, 0.000000000000000000 ) ) ;
#3383=ADVANCED_FACE ( 'NONE', ( #7672 ), #10180, .T. ) ;
#3393=EDGE_LOOP ( 'NONE', ( #12793, #3112, #5373, #10201 ) ) ;
#3396=ADVANCED_FACE ( 'NONE', ( #12352 ), #397, .T. ) ;
#3402=B_SPLINE_CURVE_WITH_KNOTS ( 'NONE', 3,
 ( #3802, #4903, #9495, #14336 ),
 .UNSPECIFIED., .F., .F.,
 ( 4, 4 ),
 ( 0.005123713096549377226, 0.005814346476695809313 ),
 .UNSPECIFIED. ) ;
#3405=CARTESIAN_POINT ( 'NONE',  ( 2.789999999999999147, 0.000000000000000000, 0.000000000000000000 ) ) ;
#3406=MECHANICAL_DESIGN_GEOMETRIC_PRESENTATION_REPRESENTATION('',(#1170),#10495);
#3407=EDGE_LOOP ( 'NONE', ( #12891, #871, #12534, #2968, #14703, #11524 ) ) ;
#3411=ORIENTED_EDGE ( 'NONE', *, *, #5994, .F. ) ;
#3414=EDGE_LOOP ( 'NONE', ( #4812, #2695, #15056, #9225 ) ) ;
#3418=DIRECTION ( 'NONE',  ( 0.000000000000000000, 0.000000000000000000, 1.000000000000000000 ) ) ;
#3430=DIRECTION ( 'NONE',  ( -1.000000000000000000, 0.000000000000000000, 0.000000000000000000 ) ) ;
#3431=DIRECTION ( 'NONE',  ( 0.000000000000000000, 0.000000000000000000, 1.000000000000000000 ) ) ;
#3442=CARTESIAN_POINT ( 'NONE',  ( 0.08941747217549800286, -14.29395843996395499, 5.279841123860813390 ) ) ;
#3451=EDGE_CURVE ( 'NONE', #14287, #10985, #12033, .T. ) ;
#3452=EDGE_CURVE ( 'NONE', #11075, #10003, #7830, .T. ) ;
#3453=CARTESIAN_POINT ( 'NONE',  ( -9.374481487433838394E-15, 2.096460570596369699, -14.05347802000166801 ) ) ;
#3456=DIRECTION ( 'NONE',  ( 0.000000000000000000, 0.000000000000000000, 1.000000000000000000 ) ) ;
#3464=EDGE_CURVE ( 'NONE', #8188, #11407, #3285, .T. ) ;
#3469=ORIENTED_EDGE ( 'NONE', *, *, #12340, .T. ) ;
#3473=VERTEX_POINT ( 'NONE', #11353 ) ;
#3477=VERTEX_POINT ( 'NONE', #3145 ) ;
#3481=CARTESIAN_POINT ( 'NONE',  ( 2.021362740937214131, 16.74220655292944926, -5.021526291670140196 ) ) ;
#3493=CARTESIAN_POINT ( 'NONE',  ( 0.5431871499410860782, -5.154374911959024530, 16.16568790143439571 ) ) ;
#3508=VERTEX_POINT ( 'NONE', #978 ) ;
#3510=ORIENTED_EDGE ( 'NONE', *, *, #11921, .F. ) ;
#3515=CARTESIAN_POINT ( 'NONE',  ( 2.582362745529149795, 10.30022894898822727, -12.04200105039459423 ) ) ;
#3527=VERTEX_POINT ( 'NONE', #10283 ) ;
#3531=CARTESIAN_POINT ( 'NONE',  ( 2.782650468023971868, 14.24968354755765709, -2.217353748341963193 ) ) ;
#3566=CIRCLE ( 'NONE', #12883, 17.95481323787947403 ) ;
#3572=CARTESIAN_POINT ( 'NONE',  ( 2.508169608347904145, 5.259531939870199402, 15.25429862889483701 ) ) ;
#3574=DIRECTION ( 'NONE',  ( 0.000000000000000000, 0.000000000000000000, 1.000000000000000000 ) ) ;
#3586=ORIENTED_EDGE ( 'NONE', *, *, #3790, .F. ) ;
#3588=CIRCLE ( 'NONE', #7024, 2.524999999999999467 ) ;
#3590=LINE ( 'NONE', #2518, #12687 ) ;
#3599=VECTOR ( 'NONE', #13887, 1000.000000000000000 ) ;
#3601=CARTESIAN_POINT ( 'NONE',  ( 8.000000000000000000, 0.000000000000000000, 0.000000000000000000 ) ) ;
#3602=EDGE_CURVE ( 'NONE', #7052, #1632, #13662, .T. ) ;
#3603=EDGE_LOOP ( 'NONE', ( #3872, #12504, #11780, #15158 ) ) ;
#3621=ADVANCED_FACE ( 'NONE', ( #2583 ), #8345, .T. ) ;
#3623=VERTEX_POINT ( 'NONE', #5904 ) ;
#3627=ORIENTED_EDGE ( 'NONE', *, *, #10373, .T. ) ;
#3636=CARTESIAN_POINT ( 'NONE',  ( 2.789999999999999147, -5.249430348645663713, -12.98979500319699731 ) ) ;
#3640=ORIENTED_EDGE ( 'NONE', *, *, #10599, .F. ) ;
#3644=VERTEX_POINT ( 'NONE', #4603 ) ;
#3656=ADVANCED_FACE ( 'NONE', ( #2509 ), #1274, .T. ) ;
#3657=CARTESIAN_POINT ( 'NONE',  ( 2.010451919658888809, 4.029281904976634188, 16.99607982911243198 ) ) ;
#3662=DIRECTION ( 'NONE',  ( -1.000000000000000000, -0.000000000000000000, -0.000000000000000000 ) ) ;
#3668=CARTESIAN_POINT ( 'NONE',  ( 0.5431870686475177568, 11.42270873787292551, 12.54666350726128243 ) ) ;
#3671=CARTESIAN_POINT ( 'NONE',  ( 1.749999999999999778, 12.55714665600005020, -12.83329210556818545 ) ) ;
#3677=AXIS2_PLACEMENT_3D ( 'NONE', #12196, #2753, #6286 ) ;
#3679=DIRECTION ( 'NONE',  ( -1.000000000000000000, -0.000000000000000000, -0.000000000000000000 ) ) ;
#3683=VERTEX_POINT ( 'NONE', #9504 ) ;
#3685=ORIENTED_EDGE ( 'NONE', *, *, #840, .T. ) ;
#3687=CARTESIAN_POINT ( 'NONE',  ( 0.07473579423048609671, 15.04916547791954606, 2.569134216958950834 ) ) ;
#3690=CARTESIAN_POINT ( 'NONE',  ( 0.9041604829517128072, -4.239993951493329583, 17.20101185193998106 ) ) ;
#3701=EDGE_CURVE ( 'NONE', #10080, #14810, #10956, .T. ) ;
#3704=CARTESIAN_POINT ( 'NONE',  ( 2.789999999999999147, -4.595504208220129172, 14.19996452731187553 ) ) ;
#3713=VERTEX_POINT ( 'NONE', #1739 ) ;
#3719=ORIENTED_EDGE ( 'NONE', *, *, #12615, .T. ) ;
#3720=CARTESIAN_POINT ( 'NONE',  ( 2.790000000000007585, 8.842327429719095022, 11.12243880662616569 ) ) ;
#3722=CIRCLE ( 'NONE', #12313, 17.95481323787947758 ) ;
#3729=DIRECTION ( 'NONE',  ( -1.000000000000000000, -0.000000000000000000, -0.000000000000000000 ) ) ;
#3731=DIRECTION ( 'NONE',  ( 0.000000000000000000, 0.000000000000000000, 1.000000000000000000 ) ) ;
#3737=EDGE_CURVE ( 'NONE', #8554, #12755, #661, .T. ) ;
#3739=ORIENTED_EDGE ( 'NONE', *, *, #1654, .T. ) ;
#3742=LINE ( 'NONE', #7060, #3865 ) ;
#3745=DIRECTION ( 'NONE',  ( -1.000000000000000000, 0.000000000000000000, 0.000000000000000000 ) ) ;
#3748=DIRECTION ( 'NONE',  ( 0.000000000000000000, 0.000000000000000000, 1.000000000000000000 ) ) ;
#3749=ORIENTED_EDGE ( 'NONE', *, *, #3084, .T. ) ;
#3750=LINE ( 'NONE', #2176, #4379 ) ;
#3751=CARTESIAN_POINT ( 'NONE',  ( 0.5537796877189875566, 11.41743294611093340, -12.52687487503407127 ) ) ;
#3754=ORIENTED_EDGE ( 'NONE', *, *, #11799, .T. ) ;
#3764=ADVANCED_FACE ( 'NONE', ( #5141 ), #9812, .T. ) ;
#3765=CARTESIAN_POINT ( 'NONE',  ( 2.508169719062757430, 12.18203740414267244, 10.58084377126627018 ) ) ;
#3778=CYLINDRICAL_SURFACE ( 'NONE', #625, 17.95481323787947403 ) ;
#3790=EDGE_CURVE ( 'NONE', #9602, #11452, #7050, .T. ) ;
#3802=CARTESIAN_POINT ( 'NONE',  ( 0.000000000000000000, -1.948757464274271767, 13.87420763704360915 ) ) ;
#3807=DIRECTION ( 'NONE',  ( -1.000000000000000000, -0.000000000000000000, -0.000000000000000000 ) ) ;
#3815=ORIENTED_EDGE ( 'NONE', *, *, #5807, .T. ) ;
#3819=CARTESIAN_POINT ( 'NONE',  ( 0.02531912748464674665, 11.36963888406700285, -9.232963481057645083 ) ) ;
#3821=FACE_OUTER_BOUND ( 'NONE', #9441, .T. ) ;
#3831=B_SPLINE_CURVE_WITH_KNOTS ( 'NONE', 3,
 ( #6342, #5434, #13490, #10104 ),
 .UNSPECIFIED., .F., .F.,
 ( 4, 4 ),
 ( 0.005123695899043907188, 0.005814329666474870977 ),
 .UNSPECIFIED. ) ;
#3834=ORIENTED_EDGE ( 'NONE', *, *, #13026, .T. ) ;
#3836=CARTESIAN_POINT ( 'NONE',  ( 0.2818302809372404405, -12.18203740414274705, 10.58084377126619025 ) ) ;
#3837=CARTESIAN_POINT ( 'NONE',  ( 0.2818303507154734100, -15.84037596932109615, 3.072260951847473720 ) ) ;
#3864=ORIENTED_EDGE ( 'NONE', *, *, #4204, .T. ) ;
#3865=VECTOR ( 'NONE', #11805, 1000.000000000000000 ) ;
#3868=ORIENTED_EDGE ( 'NONE', *, *, #3317, .T. ) ;
#3870=DIRECTION ( 'NONE',  ( 0.000000000000000000, 0.000000000000000000, 1.000000000000000000 ) ) ;
#3872=ORIENTED_EDGE ( 'NONE', *, *, #4677, .T. ) ;
#3874=DIRECTION ( 'NONE',  ( -1.000000000000000000, 0.000000000000000000, 0.000000000000000000 ) ) ;
#3875=PLANE ( 'NONE',  #2862 ) ;
#3877=AXIS2_PLACEMENT_3D ( 'NONE', #14635, #3103, #11155 ) ;
#3907=DIRECTION ( 'NONE',  ( -1.000000000000000000, -0.000000000000000000, -0.000000000000000000 ) ) ;
#3909=CARTESIAN_POINT ( 'NONE',  ( 2.560885596921109730, 15.06658931286051839, 5.279841123860919971 ) ) ;
#3919=DIRECTION ( 'NONE',  ( 0.000000000000000000, 0.000000000000000000, 1.000000000000000000 ) ) ;
#3920=ORIENTED_EDGE ( 'NONE', *, *, #12852, .F. ) ;
#3939=( NAMED_UNIT ( * ) PLANE_ANGLE_UNIT ( ) SI_UNIT ( $, .RADIAN. ) );
#3940=ORIENTED_EDGE ( 'NONE', *, *, #46, .F. ) ;
#3948=B_SPLINE_CURVE_WITH_KNOTS ( 'NONE', 3,
 ( #6904, #13590, #10291, #985, #9213, #5397, #9068, #9138 ),
 .UNSPECIFIED., .F., .F.,
 ( 4, 2, 2, 4 ),
 ( 4.663089342034314221E-07, 0.001898630032275742084, 0.002847711893946511166, 0.003796793755617280681 ),
 .UNSPECIFIED. ) ;
#3951=CARTESIAN_POINT ( 'NONE',  ( 0.02531912748286561932, 13.68080036884348516, 5.229914364928400339 ) ) ;
#3952=CARTESIAN_POINT ( 'NONE',  ( 0.02531912748679129854, 11.36963888406687317, 9.232963481057801403 ) ) ;
#3955=DIRECTION ( 'NONE',  ( -1.000000000000000000, 0.000000000000000000, -0.000000000000000000 ) ) ;
#3957=CARTESIAN_POINT ( 'NONE',  ( 0.7795480827049469097, 16.73367785739764813, -5.008579424861385299 ) ) ;
#3959=ORIENTED_EDGE ( 'NONE', *, *, #1269, .T. ) ;
#3972=ORIENTED_EDGE ( 'NONE', *, *, #13956, .T. ) ;
#3983=ORIENTED_EDGE ( 'NONE', *, *, #3602, .T. ) ;
#3991=CARTESIAN_POINT ( 'NONE',  ( 2.582362745529149795, -10.30022894898814734, 12.04200105039466528 ) ) ;
#3992=CARTESIAN_POINT ( 'NONE',  ( 0.2076373213219109837, -15.57879356040265151, 2.899259574942692819 ) ) ;
#3997=AXIS2_PLACEMENT_3D ( 'NONE', #8507, #13198, #429 ) ;
#4001=B_SPLINE_CURVE_WITH_KNOTS ( 'NONE', 3,
 ( #10442, #15060, #2147, #6834, #6908, #10214, #4533, #5618 ),
 .UNSPECIFIED., .F., .F.,
 ( 4, 2, 2, 4 ),
 ( 2.154797737799112159E-07, 0.001895231411415137677, 0.002842739377235818047, 0.003790247343056497766 ),
 .UNSPECIFIED. ) ;
#4002=ORIENTED_EDGE ( 'NONE', *, *, #2531, .F. ) ;
#4005=( NAMED_UNIT ( * ) PLANE_ANGLE_UNIT ( ) SI_UNIT ( $, .RADIAN. ) );
#4006=VERTEX_POINT ( 'NONE', #11704 ) ;
#4007=ORIENTED_EDGE ( 'NONE', *, *, #14651, .F. ) ;
#4010=CARTESIAN_POINT ( 'NONE',  ( 0.000000000000000000, -1.948757464274271767, 13.87420763704360915 ) ) ;
#4025=CARTESIAN_POINT ( 'NONE',  ( 0.2076372544708505186, 12.04200105039484825, -10.30022894898793595 ) ) ;
#4030=ORIENTED_EDGE ( 'NONE', *, *, #3737, .T. ) ;
#4032=DIRECTION ( 'NONE',  ( 1.000000000000000000, -0.000000000000000000, -0.000000000000000000 ) ) ;
#4038=CIRCLE ( 'NONE', #12848, 2.524999999999998579 ) ;
#4048=ORIENTED_EDGE ( 'NONE', *, *, #13312, .T. ) ;
#4056=DIRECTION ( 'NONE',  ( 0.000000000000000000, 0.000000000000000000, 1.000000000000000000 ) ) ;
#4062=ORIENTED_EDGE ( 'NONE', *, *, #399, .T. ) ;
#4065=CIRCLE ( 'NONE', #2331, 17.95481323787947758 ) ;
#4066=DIRECTION ( 'NONE',  ( -1.000000000000000000, -0.000000000000000000, -0.000000000000000000 ) ) ;
#4069=FACE_OUTER_BOUND ( 'NONE', #11581, .T. ) ;
#4077=CARTESIAN_POINT ( 'NONE',  ( 2.782650468023970092, 2.217353748341931663, 14.24968354755769440 ) ) ;
#4084=CIRCLE ( 'NONE', #891, 4.000000000000000000 ) ;
#4092=ORIENTED_EDGE ( 'NONE', *, *, #12642, .F. ) ;
#4096=DIRECTION ( 'NONE',  ( 0.000000000000000000, 0.000000000000000000, 1.000000000000000000 ) ) ;
#4104=CYLINDRICAL_SURFACE ( 'NONE', #12084, 2.524999999999999023 ) ;
#4106=CIRCLE ( 'NONE', #5353, 17.95481323787947758 ) ;
#4109=CARTESIAN_POINT ( 'NONE',  ( 0.4522159317772137532, 15.84984805378638484, -5.191253194755847566 ) ) ;
#4111=TOROIDAL_SURFACE ( 'NONE', #13428, 14.01039946648073986, 8.000000000000000000 ) ;
#4112=ORIENTED_EDGE ( 'NONE', *, *, #14328, .T. ) ;
#4118=EDGE_CURVE ( 'NONE', #6030, #8726, #1416, .T. ) ;
#4123=ORIENTED_EDGE ( 'NONE', *, *, #10600, .F. ) ;
#4143=CARTESIAN_POINT ( 'NONE',  ( 2.789999999999999147, 1.621424371464993087E-13, -15.47981323787947794 ) ) ;
#4145=DIRECTION ( 'NONE',  ( -1.000000000000000000, -0.000000000000000000, -0.000000000000000000 ) ) ;
#4152=CIRCLE ( 'NONE', #669, 2.524999999999999467 ) ;
#4156=EDGE_LOOP ( 'NONE', ( #9583, #3189, #2671, #11607, #13630, #1422 ) ) ;
#4161=DIRECTION ( 'NONE',  ( -1.000000000000000000, 0.000000000000000000, 0.000000000000000000 ) ) ;
#4166=CARTESIAN_POINT ( 'NONE',  ( -6.154400080602563004E-14, -11.12234047011196658, 8.842064619038488615 ) ) ;
#4169=( LENGTH_UNIT ( ) NAMED_UNIT ( * ) SI_UNIT ( .MILLI., .METRE. ) );
#4172=SHAPE_REPRESENTATION ( 'short pitch roller chain wheel_s_iso_Chain wheel ISO - 12Z 05B-1 --12SA8.0N', ( #1376 ), #13900 ) ;
#4174=AXIS2_PLACEMENT_3D ( 'NONE', #11438, #7846, #12528 ) ;
#4175=CARTESIAN_POINT ( 'NONE',  ( 0.007327564474061089815, 9.044896821682200994, 11.23174270417332465 ) ) ;
#4177=EDGE_CURVE ( 'NONE', #212, #1071, #9392, .T. ) ;
#4178=DIRECTION ( 'NONE',  ( -1.000000000000000000, 0.000000000000000000, 0.000000000000000000 ) ) ;
#4183=CIRCLE ( 'NONE', #6382, 2.524999999999999467 ) ;
#4186=ADVANCED_FACE ( 'NONE', ( #11089 ), #4104, .F. ) ;
#4190=CARTESIAN_POINT ( 'NONE',  ( 1.749999999999999778, -12.83329210556822453, -12.55714665600001290 ) ) ;
#4191=B_SPLINE_CURVE_WITH_KNOTS ( 'NONE', 3,
 ( #8826, #10900, #13439, #3836, #2693, #6146, #365, #13212 ),
 .UNSPECIFIED., .F., .F.,
 ( 4, 2, 2, 4 ),
 ( 4.663089536341708793E-07, 0.001898630414085407348, 0.002847712466651294069, 0.003796794519217180572 ),
 .UNSPECIFIED. ) ;
#4192=ORIENTED_EDGE ( 'NONE', *, *, #15179, .F. ) ;
#4194=FACE_OUTER_BOUND ( 'NONE', #3414, .T. ) ;
#4197=VERTEX_POINT ( 'NONE', #10247 ) ;
#4204=EDGE_CURVE ( 'NONE', #13954, #6351, #5721, .T. ) ;
#4211=CARTESIAN_POINT ( 'NONE',  ( 2.646101151984011857, -14.59528211758545524, 5.279841123860813390 ) ) ;
#4215=DIRECTION ( 'NONE',  ( 1.000000000000000000, 0.000000000000000000, 0.000000000000000000 ) ) ;
#4219=DIRECTION ( 'NONE',  ( 0.000000000000000000, 0.000000000000000000, 1.000000000000000000 ) ) ;
#4222=EDGE_CURVE ( 'NONE', #10087, #8808, #11565, .T. ) ;
#4225=DIRECTION ( 'NONE',  ( -1.000000000000000000, -0.000000000000000000, -0.000000000000000000 ) ) ;
#4230=CARTESIAN_POINT ( 'NONE',  ( 0.02531912748679520167, -11.36963888406680923, -9.232963481057881339 ) ) ;
#4231=CARTESIAN_POINT ( 'NONE',  ( 1.039999999999999147, -17.39253030560838198, -4.458161950358684678 ) ) ;
#4233=CARTESIAN_POINT ( 'NONE',  ( 2.789999999999999147, 14.59528211760002137, 5.279841123860918195 ) ) ;
#4237=ORIENTED_EDGE ( 'NONE', *, *, #14468, .T. ) ;
#4241=ORIENTED_EDGE ( 'NONE', *, *, #4788, .F. ) ;
#4251=CARTESIAN_POINT ( 'NONE',  ( 0.007349531976028004371, -14.24968354755767130, -2.217353748342081321 ) ) ;
#4254=LINE ( 'NONE', #12075, #2815 ) ;
#4263=ORIENTED_EDGE ( 'NONE', *, *, #5155, .F. ) ;
#4271=DIRECTION ( 'NONE',  ( -1.000000000000000000, -0.000000000000000000, -0.000000000000000000 ) ) ;
#4281=CARTESIAN_POINT ( 'NONE',  ( 2.764680872515353105, 13.68080036884348516, 5.229914364928400339 ) ) ;
#4292=CIRCLE ( 'NONE', #5036, 14.01039946648073986 ) ;
#4301=B_SPLINE_CURVE_WITH_KNOTS ( 'NONE', 3,
 ( #14464, #12053, #687, #4230 ),
 .UNSPECIFIED., .F., .F.,
 ( 4, 4 ),
 ( 0.005123695899043908056, 0.005814329666474863170 ),
 .UNSPECIFIED. ) ;
#4302=CARTESIAN_POINT ( 'NONE',  ( -6.183853848222731672E-14, -14.05326139264729335, 2.096282088614720873 ) ) ;
#4310=DIRECTION ( 'NONE',  ( -1.000000000000000000, 0.000000000000000000, -0.000000000000000000 ) ) ;
#4313=CARTESIAN_POINT ( 'NONE',  ( 2.764680872515352661, -2.311161484776655950, 14.46287784598616355 ) ) ;
#4319=ORIENTED_EDGE ( 'NONE', *, *, #9287, .T. ) ;
#4329=CARTESIAN_POINT ( 'NONE',  ( 2.789999999999999147, 8.624777288397954322, -11.04103753892262496 ) ) ;
#4332=CARTESIAN_POINT ( 'NONE',  ( 0.8341317985991834050, 16.87476974924770801, 4.976599981640402071 ) ) ;
#4334=AXIS2_PLACEMENT_3D ( 'NONE', #510, #6216, #282 ) ;
#4335=ORIENTED_EDGE ( 'NONE', *, *, #12571, .F. ) ;
#4339=ORIENTED_EDGE ( 'NONE', *, *, #11798, .F. ) ;
#4340=ORIENTED_EDGE ( 'NONE', *, *, #8959, .T. ) ;
#4344=AXIS2_PLACEMENT_3D ( 'NONE', #12137, #5407, #8759 ) ;
#4348=CARTESIAN_POINT ( 'NONE',  ( 0.01818964989807676444, -13.58893811801117124, -5.219853812241048274 ) ) ;
#4353=CARTESIAN_POINT ( 'NONE',  ( 0.7686372430964718561, 4.022333916463595394, 17.00993931356762801 ) ) ;
#4357=B_SPLINE_CURVE_WITH_KNOTS ( 'NONE', 3,
 ( #8183, #11788, #2348, #3572, #2572, #11638, #14187, #14104 ),
 .UNSPECIFIED., .F., .F.,
 ( 4, 2, 2, 4 ),
 ( 4.663089341996299912E-07, 0.001898630032275737747, 0.002847711893946506829, 0.003796793755617275910 ),
 .UNSPECIFIED. ) ;
#4359=DIRECTION ( 'NONE',  ( -1.000000000000000000, 0.000000000000000000, 0.000000000000000000 ) ) ;
#4362=CARTESIAN_POINT ( 'NONE',  ( 1.039999999999997149, -17.39253030560844948, 4.458161950358441317 ) ) ;
#4365=DIRECTION ( 'NONE',  ( 0.000000000000000000, 1.000000000000000000, 1.030528797609984825E-14 ) ) ;
#4374=AXIS2_PLACEMENT_3D ( 'NONE', #12982, #14145, #11902 ) ;
#4375=LINE ( 'NONE', #7836, #14398 ) ;
#4377=AXIS2_PLACEMENT_3D ( 'NONE', #7959, #8958, #2119 ) ;
#4379=VECTOR ( 'NONE', #7935, 1000.000000000000000 ) ;
#4383=EDGE_CURVE ( 'NONE', #13491, #8726, #3236, .T. ) ;
#4386=DIRECTION ( 'NONE',  ( -1.000000000000000000, 0.000000000000000000, -0.000000000000000000 ) ) ;
#4388=EDGE_CURVE ( 'NONE', #14287, #6222, #3008, .T. ) ;
#4389=B_SPLINE_CURVE_WITH_KNOTS ( 'NONE', 3,
 ( #6173, #11920, #5033, #1410, #9555, #6100, #238, #5194 ),
 .UNSPECIFIED., .F., .F.,
 ( 4, 2, 2, 4 ),
 ( 4.663089412874008411E-07, 0.001898630173449118675, 0.002847712105703034072, 0.003796794037956949686 ),
 .UNSPECIFIED. ) ;
#4400=ADVANCED_FACE ( 'NONE', ( #10471 ), #12666, .T. ) ;
#4401=VERTEX_POINT ( 'NONE', #11518 ) ;
#4402=ORIENTED_EDGE ( 'NONE', *, *, #13612, .F. ) ;
#4412=VERTEX_POINT ( 'NONE', #11369 ) ;
#4413=CARTESIAN_POINT ( 'NONE',  ( 2.789999999999999147, 5.249430348645756084, 12.98979500319695823 ) ) ;
#4415=ADVANCED_FACE ( 'NONE', ( #6689 ), #6841, .F. ) ;
#4416=B_SPLINE_CURVE_WITH_KNOTS ( 'NONE', 3,
 ( #3819, #9430, #11878, #9362 ),
 .UNSPECIFIED., .F., .F.,
 ( 4, 4 ),
 ( 2.451234579310872104E-07, 0.0006917187676826484820 ),
 .UNSPECIFIED. ) ;
#4425=EDGE_CURVE ( 'NONE', #10003, #6544, #1593, .T. ) ;
#4431=CARTESIAN_POINT ( 'NONE',  ( 2.764680872515353105, 13.68080036884348516, 5.229914364928400339 ) ) ;
#4452=ORIENTED_EDGE ( 'NONE', *, *, #7849, .T. ) ;
#4454=DIRECTION ( 'NONE',  ( -1.000000000000000000, -0.000000000000000000, -0.000000000000000000 ) ) ;
#4456=ORIENTED_EDGE ( 'NONE', *, *, #12002, .T. ) ;
#4457=ORIENTED_EDGE ( 'NONE', *, *, #3095, .F. ) ;
#4465=DIRECTION ( 'NONE',  ( 0.000000000000000000, 0.000000000000000000, 1.000000000000000000 ) ) ;
#4468=CARTESIAN_POINT ( 'NONE',  ( 2.246812880117043498, 16.57708379306443902, 3.619024283482126680 ) ) ;
#4488=B_SPLINE_CURVE_WITH_KNOTS ( 'NONE', 3,
 ( #5934, #7231, #14148, #12985, #9535, #2473, #3690, #11906 ),
 .UNSPECIFIED., .F., .F.,
 ( 4, 2, 2, 4 ),
 ( 2.154797737779095183E-07, 0.001895231411415135075, 0.002842739377235819782, 0.003790247343056505139 ),
 .UNSPECIFIED. ) ;
#4493=AXIS2_PLACEMENT_3D ( 'NONE', #14769, #7991, #4465 ) ;
#4495=EDGE_CURVE ( 'NONE', #11120, #6334, #8910, .T. ) ;
#4497=ORIENTED_EDGE ( 'NONE', *, *, #12434, .F. ) ;
#4503=CARTESIAN_POINT ( 'NONE',  ( 0.2076373213219092628, 2.899259574942746998, 15.57879356040263907 ) ) ;
#4505=VERTEX_POINT ( 'NONE', #12742 ) ;
#4533=CARTESIAN_POINT ( 'NONE',  ( 1.885839517048287561, -17.20101185194003790, 4.239993951493146618 ) ) ;
#4541=VECTOR ( 'NONE', #1564, 1000.000000000000000 ) ;
#4543=LINE ( 'NONE', #5771, #5269 ) ;
#4547=VERTEX_POINT ( 'NONE', #1222 ) ;
#4554=CARTESIAN_POINT ( 'NONE',  ( 2.764680872515353993, -5.229914364928256454, -13.68080036884353845 ) ) ;
#4560=CIRCLE ( 'NONE', #8707, 14.01039946648074341 ) ;
#4563=CARTESIAN_POINT ( 'NONE',  ( 0.04999671152044155020, 14.75565684666100275, -2.439987328296890468 ) ) ;
#4569=ORIENTED_EDGE ( 'NONE', *, *, #1156, .T. ) ;
#4573=CARTESIAN_POINT ( 'NONE',  ( 8.000000000000000000, 0.000000000000000000, 0.000000000000000000 ) ) ;
#4575=CARTESIAN_POINT ( 'NONE',  ( 1.749999999999999778, 0.000000000000000000, 0.000000000000000000 ) ) ;
#4577=TOROIDAL_SURFACE ( 'NONE', #13148, 14.01039946648073986, 8.000000000000000000 ) ;
#4579=ORIENTED_EDGE ( 'NONE', *, *, #8638, .T. ) ;
#4582=CARTESIAN_POINT ( 'NONE',  ( 2.782672486186223981, -13.44898112152242220, 5.204526028255641812 ) ) ;
#4589=CARTESIAN_POINT ( 'NONE',  ( 2.789999999999999147, 14.46287784598617243, 2.311161484776605324 ) ) ;
#4590=DIRECTION ( 'NONE',  ( 0.000000000000000000, 6.870191984066565499E-15, -1.000000000000000000 ) ) ;
#4591=VECTOR ( 'NONE', #4787, 1000.000000000000000 ) ;
#4601=DIRECTION ( 'NONE',  ( 0.000000000000000000, 0.000000000000000000, 1.000000000000000000 ) ) ;
#4602=DIRECTION ( 'NONE',  ( 0.000000000000000000, 0.000000000000000000, 1.000000000000000000 ) ) ;
#4603=CARTESIAN_POINT ( 'NONE',  ( 2.764680872515352661, 5.229914364928351489, 13.68080036884350292 ) ) ;
#4615=CARTESIAN_POINT ( 'NONE',  ( 0.002676282549904213624, -13.26666194250858233, -5.214906618938926819 ) ) ;
#4616=CYLINDRICAL_SURFACE ( 'NONE', #8537, 17.95481323787947403 ) ;
#4619=CARTESIAN_POINT ( 'NONE',  ( 0.02531912748464718033, -14.46287784598619020, 2.311161484776505404 ) ) ;
#4625=ORIENTED_EDGE ( 'NONE', *, *, #6578, .T. ) ;
#4631=AXIS2_PLACEMENT_3D ( 'NONE', #2461, #3679, #5712 ) ;
#4636=DIRECTION ( 'NONE',  ( -1.000000000000000000, 0.000000000000000000, -0.000000000000000000 ) ) ;
#4639=CARTESIAN_POINT ( 'NONE',  ( 0.02531912748464718033, -9.232963481057685939, -11.36963888406697087 ) ) ;
#4641=CARTESIAN_POINT ( 'NONE',  ( 0.2818303507154722998, -3.072260951847419097, -15.84037596932111036 ) ) ;
#4647=AXIS2_PLACEMENT_3D ( 'NONE', #14344, #3807, #14508 ) ;
#4651=CARTESIAN_POINT ( 'NONE',  ( 2.782650442329440477, 11.23191127083875962, -9.045126717605661781 ) ) ;
#4653=ORIENTED_EDGE ( 'NONE', *, *, #14230, .T. ) ;
#4656=ORIENTED_EDGE ( 'NONE', *, *, #4177, .T. ) ;
#4659=TOROIDAL_SURFACE ( 'NONE', #14964, 14.01039946648073986, 8.000000000000000000 ) ;
#4660=ADVANCED_FACE ( 'NONE', ( #3821 ), #10747, .T. ) ;
#4666=CARTESIAN_POINT ( 'NONE',  ( 0.9041604829517113640, 4.239993951493447710, -17.20101185193995974 ) ) ;
#4677=EDGE_CURVE ( 'NONE', #2043, #12774, #12749, .T. ) ;
#4684=ORIENTED_EDGE ( 'NONE', *, *, #5091, .T. ) ;
#4685=B_SPLINE_CURVE_WITH_KNOTS ( 'NONE', 3,
 ( #11700, #1034, #7104, #10402, #1187, #3338, #13864, #8326 ),
 .UNSPECIFIED., .F., .F.,
 ( 4, 2, 2, 4 ),
 ( 4.663089341997027831E-07, 0.001440500229357419932, 0.002160517189569030432, 0.002880534149780641148 ),
 .UNSPECIFIED. ) ;
#4686=ORIENTED_EDGE ( 'NONE', *, *, #13956, .F. ) ;
#4689=B_SPLINE_CURVE_WITH_KNOTS ( 'NONE', 3,
 ( #13700, #11535, #4251, #10316 ),
 .UNSPECIFIED., .F., .F.,
 ( 4, 4 ),
 ( 0.005123713096549378093, 0.005814346476695809313 ),
 .UNSPECIFIED. ) ;
#4708=CARTESIAN_POINT ( 'NONE',  ( 0.4522159317772141973, -5.191253194755903522, -15.84984805378637063 ) ) ;
#4712=ADVANCED_FACE ( 'NONE', ( #14359 ), #8588, .F. ) ;
#4717=EDGE_CURVE ( 'NONE', #5935, #14375, #1021, .T. ) ;
#4718=ORIENTED_EDGE ( 'NONE', *, *, #4776, .T. ) ;
#4727=DIRECTION ( 'NONE',  ( 1.000000000000000000, 0.000000000000000000, 0.000000000000000000 ) ) ;
#4736=ORIENTED_EDGE ( 'NONE', *, *, #14171, .F. ) ;
#4738=CARTESIAN_POINT ( 'NONE',  ( 2.789999999999999147, 13.87420763704361093, -1.948757464274220697 ) ) ;
#4739=CARTESIAN_POINT ( 'NONE',  ( 2.764680872515352217, 14.46287784598617243, 2.311161484776605324 ) ) ;
#4745=CARTESIAN_POINT ( 'NONE',  ( 2.789999999999999147, -13.68080036884352246, 5.229914364928304416 ) ) ;
#4748=CARTESIAN_POINT ( 'NONE',  ( 2.789999999999999147, 0.000000000000000000, 0.000000000000000000 ) ) ;
#4751=EDGE_LOOP ( 'NONE', ( #1213, #6500, #11107, #7625, #14080, #14774, #3834, #14011 ) ) ;
#4769=B_SPLINE_CURVE_WITH_KNOTS ( 'NONE', 3,
 ( #14025, #2346, #3493, #8181, #1197, #2426, #5891, #10573 ),
 .UNSPECIFIED., .F., .F.,
 ( 4, 2, 2, 4 ),
 ( 4.663089341996299912E-07, 0.001898630032275737097, 0.002847711893946505961, 0.003796793755617274609 ),
 .UNSPECIFIED. ) ;
#4774=ORIENTED_EDGE ( 'NONE', *, *, #8675, .T. ) ;
#4776=EDGE_CURVE ( 'NONE', #9529, #3101, #890, .T. ) ;
#4780=FACE_OUTER_BOUND ( 'NONE', #9358, .T. ) ;
#4787=DIRECTION ( 'NONE',  ( -1.000000000000000000, 0.000000000000000000, 0.000000000000000000 ) ) ;
#4788=EDGE_CURVE ( 'NONE', #3473, #1894, #13974, .T. ) ;
#4796=EDGE_CURVE ( 'NONE', #3644, #5314, #8884, .T. ) ;
#4802=EDGE_CURVE ( 'NONE', #8896, #228, #3178, .T. ) ;
#4803=VERTEX_POINT ( 'NONE', #3139 ) ;
#4807=CARTESIAN_POINT ( 'NONE',  ( 1.394999999999998685, -4.458161950358380921, -17.39253030560846369 ) ) ;
#4812=ORIENTED_EDGE ( 'NONE', *, *, #936, .T. ) ;
#4814=CARTESIAN_POINT ( 'NONE',  ( 0.02531912748679520167, -11.36963888406680923, -9.232963481057881339 ) ) ;
#4840=LINE ( 'NONE', #13984, #5422 ) ;
#4844=AXIS2_PLACEMENT_3D ( 'NONE', #12797, #12871, #2285 ) ;
#4847=ADVANCED_FACE ( 'NONE', ( #5450 ), #4659, .T. ) ;
#4848=ORIENTED_EDGE ( 'NONE', *, *, #4177, .F. ) ;
#4852=AXIS2_PLACEMENT_3D ( 'NONE', #11676, #10609, #1237 ) ;
#4859=EDGE_CURVE ( 'NONE', #2773, #14197, #831, .T. ) ;
#4860=CARTESIAN_POINT ( 'NONE',  ( 2.764680872515351329, 14.46287784598617421, -2.311161484776606212 ) ) ;
#4863=CARTESIAN_POINT ( 'NONE',  ( 2.582362745529150683, 12.04200105039470259, 10.30022894898810293 ) ) ;
#4865=DIRECTION ( 'NONE',  ( 0.000000000000000000, 0.000000000000000000, 1.000000000000000000 ) ) ;
#4873=CARTESIAN_POINT ( 'NONE',  ( 0.09203968221122160731, -14.31435947614538406, -5.280991956247265584 ) ) ;
#4877=AXIS2_PLACEMENT_3D ( 'NONE', #7801, #14726, #643 ) ;
#4878=CARTESIAN_POINT ( 'NONE',  ( 0.000000000000000000, 0.000000000000000000, 0.000000000000000000 ) ) ;
#4881=DIRECTION ( 'NONE',  ( -1.000000000000000000, 0.000000000000000000, 0.000000000000000000 ) ) ;
#4888=ORIENTED_EDGE ( 'NONE', *, *, #12204, .T. ) ;
#4889=TOROIDAL_SURFACE ( 'NONE', #12720, 14.01039946648074341, 8.000000000000000000 ) ;
#4903=CARTESIAN_POINT ( 'NONE',  ( -1.093979827056220885E-14, -2.096460570596271111, 14.05347802000168400 ) ) ;
#4908=DIRECTION ( 'NONE',  ( 0.000000000000000000, 0.000000000000000000, 1.000000000000000000 ) ) ;
#4914=ORIENTED_EDGE ( 'NONE', *, *, #5548, .T. ) ;
#4926=VERTEX_POINT ( 'NONE', #971 ) ;
#4928=CARTESIAN_POINT ( 'NONE',  ( 0.1920562174424401414, 10.28947301956298865, -12.05486625177560711 ) ) ;
#4930=EDGE_CURVE ( 'NONE', #6544, #7716, #6119, .T. ) ;
#4933=VERTEX_POINT ( 'NONE', #8185 ) ;
#4947=DIRECTION ( 'NONE',  ( 0.000000000000000000, 0.000000000000000000, 1.000000000000000000 ) ) ;
#4951=FACE_OUTER_BOUND ( 'NONE', #5911, .T. ) ;
#4952=ORIENTED_EDGE ( 'NONE', *, *, #7230, .T. ) ;
#4963=ORIENTED_EDGE ( 'NONE', *, *, #130, .T. ) ;
#4964=ORIENTED_EDGE ( 'NONE', *, *, #8428, .F. ) ;
#4967=ADVANCED_FACE ( 'NONE', ( #9126 ), #957, .T. ) ;
#4968=EDGE_CURVE ( 'NONE', #3623, #9188, #9199, .T. ) ;
#4974=ORIENTED_EDGE ( 'NONE', *, *, #540, .F. ) ;
#4976=CARTESIAN_POINT ( 'NONE',  ( 1.749999999999999778, 0.000000000000000000, 0.000000000000000000 ) ) ;
#4977=CARTESIAN_POINT ( 'NONE',  ( 2.236220346785029012, -3.624349476775082124, -16.55730827443884934 ) ) ;
#4986=ORIENTED_EDGE ( 'NONE', *, *, #9304, .F. ) ;
#5012=CARTESIAN_POINT ( 'NONE',  ( 0.9041604829517133624, 17.20101185194000593, 4.239993951493269186 ) ) ;
#5019=EDGE_CURVE ( 'NONE', #9188, #3101, #8812, .T. ) ;
#5024=EDGE_CURVE ( 'NONE', #8726, #8554, #12563, .T. ) ;
#5028=VECTOR ( 'NONE', #15152, 1000.000000000000000 ) ;
#5033=CARTESIAN_POINT ( 'NONE',  ( 2.246812880117043942, -16.57708379306441415, -3.619024283482240811 ) ) ;
#5036=AXIS2_PLACEMENT_3D ( 'NONE', #6306, #5241, #2702 ) ;
#5043=ADVANCED_FACE ( 'NONE', ( #1124 ), #5824, .T. ) ;
#5055=CARTESIAN_POINT ( 'NONE',  ( 2.764680872513935128, -5.229914364928447412, 13.68080036884346917 ) ) ;
#5076=EDGE_CURVE ( 'NONE', #8949, #3508, #3402, .T. ) ;
#5077=ORIENTED_EDGE ( 'NONE', *, *, #14900, .T. ) ;
#5083=EDGE_LOOP ( 'NONE', ( #13036, #2139, #11933, #13320 ) ) ;
#5091=EDGE_CURVE ( 'NONE', #12774, #10832, #6621, .T. ) ;
#5092=CARTESIAN_POINT ( 'NONE',  ( 2.790000000000061764, 8.842064619038678686, -11.12234047011180849 ) ) ;
#5093=CARTESIAN_POINT ( 'NONE',  ( 2.715264245299034762, -9.749517823373922809, -11.74839219818098535 ) ) ;
#5096=CIRCLE ( 'NONE', #12908, 14.01039946648073986 ) ;
#5098=EDGE_LOOP ( 'NONE', ( #9928, #3739, #14775, #15220 ) ) ;
#5102=AXIS2_PLACEMENT_3D ( 'NONE', #7961, #11567, #1901 ) ;
#5103=FILL_AREA_STYLE ('',( #11072 ) ) ;
#5107=DIRECTION ( 'NONE',  ( 0.000000000000000000, 0.000000000000000000, 1.000000000000000000 ) ) ;
#5108=CARTESIAN_POINT ( 'NONE',  ( 0.04999671820202237355, -13.99876742897255255, -5.264737421541672013 ) ) ;
#5116=CARTESIAN_POINT ( 'NONE',  ( 0.1438988480159978933, 14.59528211758547478, 5.279841123860917307 ) ) ;
#5135=CIRCLE ( 'NONE', #11245, 4.000000000000000000 ) ;
#5141=FACE_OUTER_BOUND ( 'NONE', #8308, .T. ) ;
#5142=ORIENTED_EDGE ( 'NONE', *, *, #12019, .F. ) ;
#5148=FACE_OUTER_BOUND ( 'NONE', #10538, .T. ) ;
#5152=CARTESIAN_POINT ( 'NONE',  ( -7.666496192563591389E-15, 11.12243880662613371, 8.842327429719135878 ) ) ;
#5155=EDGE_CURVE ( 'NONE', #9636, #1316, #6189, .T. ) ;
#5156=ORIENTED_EDGE ( 'NONE', *, *, #5165, .T. ) ;
#5157=DIRECTION ( 'NONE',  ( 0.000000000000000000, 0.000000000000000000, 1.000000000000000000 ) ) ;
#5158=CARTESIAN_POINT ( 'NONE',  ( 2.764680872515351773, 11.36963888406687317, 9.232963481057801403 ) ) ;
#5165=EDGE_CURVE ( 'NONE', #5688, #3069, #12732, .T. ) ;
#5167=FACE_OUTER_BOUND ( 'NONE', #2936, .T. ) ;
#5176=LINE ( 'NONE', #9844, #11396 ) ;
#5185=ADVANCED_FACE ( 'NONE', ( #13175 ), #8088, .T. ) ;
#5189=ADVANCED_FACE ( 'NONE', ( #14628 ), #14714, .T. ) ;
#5192=ORIENTED_EDGE ( 'NONE', *, *, #14364, .T. ) ;
#5194=CARTESIAN_POINT ( 'NONE',  ( 2.764680872515352661, -14.46287784598615644, -2.311161484776706576 ) ) ;
#5195=EDGE_CURVE ( 'NONE', #2455, #13761, #11271, .T. ) ;
#5199=ORIENTED_EDGE ( 'NONE', *, *, #14220, .T. ) ;
#5205=FACE_OUTER_BOUND ( 'NONE', #5289, .T. ) ;
#5210=DIRECTION ( 'NONE',  ( 0.000000000000000000, 0.000000000000000000, -1.000000000000000000 ) ) ;
#5213=CARTESIAN_POINT ( 'NONE',  ( 2.789999999999999147, 9.999777909379933050, 11.07980565117283689 ) ) ;
#5215=ORIENTED_EDGE ( 'NONE', *, *, #6838, .F. ) ;
#5223=CARTESIAN_POINT ( 'NONE',  ( 2.789999999999999147, -14.59528211760000005, -3.120158876139185189 ) ) ;
#5225=CARTESIAN_POINT ( 'NONE',  ( 2.789999999999999147, -13.40591150984221080, -7.739906618939849103 ) ) ;
#5230=CARTESIAN_POINT ( 'NONE',  ( -6.124749847962873057E-14, -5.211197193340786349, 13.21862218141514411 ) ) ;
#5232=CARTESIAN_POINT ( 'NONE',  ( 2.764680872515352661, -9.232963481057844035, 11.36963888406684298 ) ) ;
#5241=DIRECTION ( 'NONE',  ( -1.000000000000000000, -0.000000000000000000, -0.000000000000000000 ) ) ;
#5244=ORIENTED_EDGE ( 'NONE', *, *, #2417, .T. ) ;
#5249=EDGE_CURVE ( 'NONE', #12118, #2773, #2850, .T. ) ;
#5257=DIRECTION ( 'NONE',  ( 0.000000000000000000, 0.000000000000000000, 1.000000000000000000 ) ) ;
#5267=EDGE_CURVE ( 'NONE', #6623, #11577, #4689, .T. ) ;
#5268=DIRECTION ( 'NONE',  ( -0.000000000000000000, 0.000000000000000000, 1.000000000000000000 ) ) ;
#5269=VECTOR ( 'NONE', #10452, 1000.000000000000000 ) ;
#5281=AXIS2_PLACEMENT_3D ( 'NONE', #7985, #13902, #8066 ) ;
#5286=B_SPLINE_CURVE_WITH_KNOTS ( 'NONE', 3,
 ( #12398, #1796, #14564, #4109, #553, #3957, #7713, #8632 ),
 .UNSPECIFIED., .F., .F.,
 ( 4, 2, 2, 4 ),
 ( 1.984117563342395502E-07, 0.001895214258086350351, 0.002842722181251363528, 0.003790230104416376488 ),
 .UNSPECIFIED. ) ;
#5289=EDGE_LOOP ( 'NONE', ( #508, #9000, #8416, #13275 ) ) ;
#5290=ORIENTED_EDGE ( 'NONE', *, *, #14032, .T. ) ;
#5293=EDGE_LOOP ( 'NONE', ( #14237, #10622, #6350, #5684 ) ) ;
#5297=FACE_OUTER_BOUND ( 'NONE', #12028, .T. ) ;
#5299=DIRECTION ( 'NONE',  ( -1.000000000000000000, -0.000000000000000000, -0.000000000000000000 ) ) ;
#5301=FACE_OUTER_BOUND ( 'NONE', #7013, .T. ) ;
#5308=CARTESIAN_POINT ( 'NONE',  ( 0.02531912748464587928, -5.229914364928447412, 13.68080036884346917 ) ) ;
#5312=DIRECTION ( 'NONE',  ( -1.000000000000000000, 0.000000000000000000, -0.000000000000000000 ) ) ;
#5314=VERTEX_POINT ( 'NONE', #8925 ) ;
#5317=CYLINDRICAL_SURFACE ( 'NONE', #9267, 8.400000000000000355 ) ;
#5344=ADVANCED_FACE ( 'NONE', ( #5487 ), #10159, .T. ) ;
#5353=AXIS2_PLACEMENT_3D ( 'NONE', #8001, #12681, #777 ) ;
#5362=EDGE_CURVE ( 'NONE', #12400, #9201, #2665, .T. ) ;
#5365=EDGE_CURVE ( 'NONE', #1234, #14323, #7427, .T. ) ;
#5366=CARTESIAN_POINT ( 'NONE',  ( 2.789999999999999147, 7.739906618939895289, -10.88091150984218380 ) ) ;
#5370=CARTESIAN_POINT ( 'NONE',  ( 1.394999999999999574, 17.29145405592688789, 4.835383649608534284 ) ) ;
#5373=ORIENTED_EDGE ( 'NONE', *, *, #14707, .T. ) ;
#5374=DIRECTION ( 'NONE',  ( 0.000000000000000000, -0.5000000000000007772, 0.8660254037844381525 ) ) ;
#5375=ORIENTED_EDGE ( 'NONE', *, *, #13221, .F. ) ;
#5381=DIRECTION ( 'NONE',  ( 0.000000000000000000, 0.000000000000000000, 1.000000000000000000 ) ) ;
#5384=CARTESIAN_POINT ( 'NONE',  ( 2.697960317788776319, 14.31435947614549242, -5.280991956246970709 ) ) ;
#5394=DIRECTION ( 'NONE',  ( -1.000000000000000000, -0.000000000000000000, -0.000000000000000000 ) ) ;
#5397=CARTESIAN_POINT ( 'NONE',  ( 0.09203968221122159343, 5.280991956247319763, -14.31435947614536275 ) ) ;
#5398=DIRECTION ( 'NONE',  ( 0.000000000000000000, 0.000000000000000000, 1.000000000000000000 ) ) ;
#5402=DIRECTION ( 'NONE',  ( 0.000000000000000000, -0.8660254037844362651, -0.5000000000000041078 ) ) ;
#5404=AXIS2_PLACEMENT_3D ( 'NONE', #5672, #8261, #1267 ) ;
#5407=DIRECTION ( 'NONE',  ( 1.000000000000000000, 0.000000000000000000, 0.000000000000000000 ) ) ;
#5410=ORIENTED_EDGE ( 'NONE', *, *, #9336, .F. ) ;
#5411=ORIENTED_EDGE ( 'NONE', *, *, #7638, .F. ) ;
#5417=EDGE_CURVE ( 'NONE', #9595, #11083, #6001, .T. ) ;
#5422=VECTOR ( 'NONE', #3380, 1000.000000000000000 ) ;
#5423=CARTESIAN_POINT ( 'NONE',  ( 1.039999999999997815, 17.29145405592688789, 4.835383649608532508 ) ) ;
#5425=ORIENTED_EDGE ( 'NONE', *, *, #2129, .F. ) ;
#5426=CARTESIAN_POINT ( 'NONE',  ( 0.02531912748464674665, -11.36963888406694068, 9.232963481057725019 ) ) ;
#5427=CARTESIAN_POINT ( 'NONE',  ( 2.582362745529150683, -12.04200105039462976, -10.30022894898818464 ) ) ;
#5434=CARTESIAN_POINT ( 'NONE',  ( 2.790000000000008029, -8.842327429719018639, -11.12243880662622431 ) ) ;
#5435=VERTEX_POINT ( 'NONE', #5865 ) ;
#5440=CARTESIAN_POINT ( 'NONE',  ( 0.2818303507154712451, 3.072260951847531008, 15.84037596932109615 ) ) ;
#5443=EDGE_CURVE ( 'NONE', #3508, #6870, #4488, .T. ) ;
#5448=CARTESIAN_POINT ( 'NONE',  ( 2.740740100656034794, 13.98927362834316135, 5.263697681271602313 ) ) ;
#5450=FACE_OUTER_BOUND ( 'NONE', #528, .T. ) ;
#5454=CARTESIAN_POINT ( 'NONE',  ( 2.740003288479521792, 2.439987328297174241, -14.75565684666123900 ) ) ;
#5478=SHAPE_REPRESENTATION_RELATIONSHIP ( 'NONE' , 'NONE' ,  #4172, #476 ) ;
#5481=ORIENTED_EDGE ( 'NONE', *, *, #8836, .F. ) ;
#5487=FACE_OUTER_BOUND ( 'NONE', #6643, .T. ) ;
#5490=AXIS2_PLACEMENT_3D ( 'NONE', #13245, #2725, #12245 ) ;
#5497=CARTESIAN_POINT ( 'NONE',  ( 2.764680872515351329, -11.36963888406680923, -9.232963481057881339 ) ) ;
#5499=VERTEX_POINT ( 'NONE', #14470 ) ;
#5502=ORIENTED_EDGE ( 'NONE', *, *, #5195, .F. ) ;
#5507=CARTESIAN_POINT ( 'NONE',  ( 0.02531912748464631296, -13.68080036884344963, -5.229914364928496262 ) ) ;
#5516=CARTESIAN_POINT ( 'NONE',  ( 2.764680872515354881, -13.68080036884352246, 5.229914364928304416 ) ) ;
#5526=EDGE_CURVE ( 'NONE', #9636, #1932, #242, .T. ) ;
#5533=DIRECTION ( 'NONE',  ( 0.000000000000000000, 0.000000000000000000, -1.000000000000000000 ) ) ;
#5548=EDGE_CURVE ( 'NONE', #406, #3713, #13489, .T. ) ;
#5551=VERTEX_POINT ( 'NONE', #6227 ) ;
#5556=ORIENTED_EDGE ( 'NONE', *, *, #5526, .T. ) ;
#5557=EDGE_LOOP ( 'NONE', ( #3749, #6480, #13478, #15007, #617, #435, #10761, #6393 ) ) ;
#5563=AXIS2_PLACEMENT_3D ( 'NONE', #13892, #5394, #6825 ) ;
#5569=AXIS2_PLACEMENT_3D ( 'NONE', #13277, #7528, #10824 ) ;
#5582=CARTESIAN_POINT ( 'NONE',  ( 2.782650468023970092, -2.217353748341832187, -14.24968354755770861 ) ) ;
#5588=VECTOR ( 'NONE', #9588, 1000.000000000000000 ) ;
#5592=ORIENTED_EDGE ( 'NONE', *, *, #2417, .F. ) ;
#5596=AXIS2_PLACEMENT_3D ( 'NONE', #10358, #3374, #7981 ) ;
#5600=DIRECTION ( 'NONE',  ( -1.000000000000000000, 0.000000000000000000, 0.000000000000000000 ) ) ;
#5608=ORIENTED_EDGE ( 'NONE', *, *, #8638, .F. ) ;
#5612=AXIS2_PLACEMENT_3D ( 'NONE', #2603, #207, #14945 ) ;
#5615=DIRECTION ( 'NONE',  ( 0.000000000000000000, 0.000000000000000000, 1.000000000000000000 ) ) ;
#5618=CARTESIAN_POINT ( 'NONE',  ( 1.749999999999999778, -17.39253030560844948, 4.458161950358431547 ) ) ;
#5623=VERTEX_POINT ( 'NONE', #14998 ) ;
#5624=CARTESIAN_POINT ( 'NONE',  ( 2.764680872515352661, -9.232963481057844035, 11.36963888406684298 ) ) ;
#5633=ORIENTED_EDGE ( 'NONE', *, *, #12845, .T. ) ;
#5634=CARTESIAN_POINT ( 'NONE',  ( 0.000000000000000000, -5.249430348645662825, -12.98979500319700264 ) ) ;
#5635=ADVANCED_FACE ( 'NONE', ( #8987 ), #14973, .T. ) ;
#5637=ADVANCED_FACE ( 'NONE', ( #838 ), #768, .T. ) ;
#5642=CARTESIAN_POINT ( 'NONE',  ( -9.203569561072644802E-15, -8.842327429719173182, 11.12243880662610529 ) ) ;
#5651=DIRECTION ( 'NONE',  ( 0.000000000000000000, 0.000000000000000000, 1.000000000000000000 ) ) ;
#5653=EDGE_CURVE ( 'NONE', #2383, #14287, #7604, .T. ) ;
#5655=EDGE_LOOP ( 'NONE', ( #15193, #6229, #4112, #13043, #288, #4030, #2666, #12822 ) ) ;
#5658=EDGE_CURVE ( 'NONE', #393, #8452, #6370, .T. ) ;
#5661=FACE_OUTER_BOUND ( 'NONE', #7952, .T. ) ;
#5672=CARTESIAN_POINT ( 'NONE',  ( 0.000000000000000000, -7.739906618939614624, -13.40591150984234581 ) ) ;
#5676=CARTESIAN_POINT ( 'NONE',  ( 2.789999999999999147, -7.739906618939802918, 13.40591150984224100 ) ) ;
#5679=ORIENTED_EDGE ( 'NONE', *, *, #14557, .F. ) ;
#5684=ORIENTED_EDGE ( 'NONE', *, *, #8821, .F. ) ;
#5688=VERTEX_POINT ( 'NONE', #12665 ) ;
#5698=ORIENTED_EDGE ( 'NONE', *, *, #1121, .F. ) ;
#5702=EDGE_LOOP ( 'NONE', ( #8017, #10409, #12030, #9755 ) ) ;
#5706=CARTESIAN_POINT ( 'NONE',  ( 1.039999999999996483, -12.55714665599978375, -12.83329210556844835 ) ) ;
#5708=UNCERTAINTY_MEASURE_WITH_UNIT (LENGTH_MEASURE( 1.000000000000000082E-05 ), #13836, 'distance_accuracy_value', 'NONE');
#5711=CARTESIAN_POINT ( 'NONE',  ( 0.008751532933531189218, -13.40591150985895297, -5.214906618939850524 ) ) ;
#5712=DIRECTION ( 'NONE',  ( 0.000000000000000000, 0.000000000000000000, 1.000000000000000000 ) ) ;
#5720=ORIENTED_EDGE ( 'NONE', *, *, #14484, .F. ) ;
#5721=CIRCLE ( 'NONE', #2985, 2.524999999999997691 ) ;
#5728=ADVANCED_FACE ( 'NONE', ( #204 ), #7860, .T. ) ;
#5729=CARTESIAN_POINT ( 'NONE',  ( 1.039999999999997593, 0.000000000000000000, 0.000000000000000000 ) ) ;
#5731=EDGE_LOOP ( 'NONE', ( #829, #12656, #15159, #10125 ) ) ;
#5733=CARTESIAN_POINT ( 'NONE',  ( 0.7795480803411087845, 4.029281904976870443, -16.99607982911238224 ) ) ;
#5746=CARTESIAN_POINT ( 'NONE',  ( -10.00000000000000000, 0.000000000000000000, 0.000000000000000000 ) ) ;
#5751=CARTESIAN_POINT ( 'NONE',  ( 2.337784068222784839, -15.84984805378628003, -5.191253194756180633 ) ) ;
#5753=EDGE_LOOP ( 'NONE', ( #8064, #12484 ) ) ;
#5757=CARTESIAN_POINT ( 'NONE',  ( -10.00000000000000000, 0.000000000000000000, 0.000000000000000000 ) ) ;
#5771=CARTESIAN_POINT ( 'NONE',  ( 2.789999999999999147, -2.311161484776455222, -14.46287784598619908 ) ) ;
#5772=EDGE_CURVE ( 'NONE', #5808, #4547, #4840, .T. ) ;
#5773=ORIENTED_EDGE ( 'NONE', *, *, #14027, .T. ) ;
#5774=B_SPLINE_CURVE_WITH_KNOTS ( 'NONE', 3,
 ( #8276, #14276, #3668, #12959, #6052, #9296, #2448, #11803 ),
 .UNSPECIFIED., .F., .F.,
 ( 4, 2, 2, 4 ),
 ( 4.663089536307853416E-07, 0.001898630414085407999, 0.002847712466651292768, 0.003796794519217177970 ),
 .UNSPECIFIED. ) ;
#5784=EDGE_CURVE ( 'NONE', #1071, #13456, #1406, .T. ) ;
#5791=DIRECTION ( 'NONE',  ( 0.000000000000000000, 0.000000000000000000, 1.000000000000000000 ) ) ;
#5792=ORIENTED_EDGE ( 'NONE', *, *, #14622, .T. ) ;
#5797=AXIS2_PLACEMENT_3D ( 'NONE', #8744, #7534, #2694 ) ;
#5807=EDGE_CURVE ( 'NONE', #6544, #11663, #7113, .T. ) ;
#5808=VERTEX_POINT ( 'NONE', #2371 ) ;
#5809=CIRCLE ( 'NONE', #6041, 17.95481323787947758 ) ;
#5814=VERTEX_POINT ( 'NONE', #8285 ) ;
#5816=DIRECTION ( 'NONE',  ( 1.000000000000000000, 0.000000000000000000, 0.000000000000000000 ) ) ;
#5821=FACE_OUTER_BOUND ( 'NONE', #2731, .T. ) ;
#5824=CYLINDRICAL_SURFACE ( 'NONE', #5873, 8.400000000000000355 ) ;
#5826=CARTESIAN_POINT ( 'NONE',  ( 2.715264205769514660, 2.569134216958901984, 15.04916547791955317 ) ) ;
#5828=VERTEX_POINT ( 'NONE', #506 ) ;
#5839=DIRECTION ( 'NONE',  ( 1.000000000000000000, 0.000000000000000000, -0.000000000000000000 ) ) ;
#5858=CARTESIAN_POINT ( 'NONE',  ( 0.6538474904312574498, -16.44008199387302582, 5.087730618022520801 ) ) ;
#5860=B_SPLINE_CURVE_WITH_KNOTS ( 'NONE', 3,
 ( #7807, #2961, #3199, #11178 ),
 .UNSPECIFIED., .F., .F.,
 ( 4, 4 ),
 ( 2.451234579310841928E-07, 0.0006917187676826554209 ),
 .UNSPECIFIED. ) ;
#5865=CARTESIAN_POINT ( 'NONE',  ( 1.749999999999999778, 4.458161950358502601, 17.39253030560843172 ) ) ;
#5873=AXIS2_PLACEMENT_3D ( 'NONE', #14031, #9409, #15207 ) ;
#5875=ADVANCED_FACE ( 'NONE', ( #10820 ), #9889, .T. ) ;
#5876=CARTESIAN_POINT ( 'NONE',  ( 0.02531912748256377743, 14.46287784598617421, -2.311161484776606212 ) ) ;
#5891=CARTESIAN_POINT ( 'NONE',  ( 0.04999671820202085393, -5.264737421541620499, 13.99876742897257742 ) ) ;
#5899=ORIENTED_EDGE ( 'NONE', *, *, #9777, .F. ) ;
#5902=CARTESIAN_POINT ( 'NONE',  ( -1.033036732025934469E-14, 5.211150952915363455, 13.21889893246977543 ) ) ;
#5904=CARTESIAN_POINT ( 'NONE',  ( 2.790000000000000924, 0.000000000000000000, 4.000000000000000000 ) ) ;
#5906=EDGE_CURVE ( 'NONE', #3044, #5828, #477, .T. ) ;
#5911=EDGE_LOOP ( 'NONE', ( #12756, #3225, #8899, #4684 ) ) ;
#5914=CARTESIAN_POINT ( 'NONE',  ( 0.9041604898882313890, 4.928563447326288482, 17.01651022436365324 ) ) ;
#5918=DIRECTION ( 'NONE',  ( -1.000000000000000000, -0.000000000000000000, -0.000000000000000000 ) ) ;
#5919=EDGE_CURVE ( 'NONE', #13214, #1249, #12112, .T. ) ;
#5925=EDGE_LOOP ( 'NONE', ( #14222, #13608, #11895, #6031, #3983, #14498 ) ) ;
#5934=CARTESIAN_POINT ( 'NONE',  ( 0.02531912748631078014, -2.311161484776655950, 14.46287784598616355 ) ) ;
#5935=VERTEX_POINT ( 'NONE', #8510 ) ;
#5941=ORIENTED_EDGE ( 'NONE', *, *, #8187, .T. ) ;
#5945=CARTESIAN_POINT ( 'NONE',  ( 0.007349531976027577629, 14.24968354755768729, 2.217353748341981401 ) ) ;
#5972=B_SPLINE_CURVE_WITH_KNOTS ( 'NONE', 3,
 ( #2075, #11443, #4468, #11301, #2157, #6843, #13600, #14841 ),
 .UNSPECIFIED., .F., .F.,
 ( 4, 2, 2, 4 ),
 ( 4.663089413084687740E-07, 0.001898630173449139926, 0.002847712105703055756, 0.003796794037956971370 ),
 .UNSPECIFIED. ) ;
#5975=CARTESIAN_POINT ( 'NONE',  ( 2.764680872515353105, 13.68080036884348516, 5.229914364928400339 ) ) ;
#5982=EDGE_LOOP ( 'NONE', ( #10636, #13358, #8216, #9403 ) ) ;
#5989=AXIS2_PLACEMENT_3D ( 'NONE', #9554, #4881, #1252 ) ;
#5991=ORIENTED_EDGE ( 'NONE', *, *, #6365, .F. ) ;
#5993=FACE_OUTER_BOUND ( 'NONE', #11433, .T. ) ;
#5994=EDGE_CURVE ( 'NONE', #3142, #5499, #4183, .T. ) ;
#5996=CARTESIAN_POINT ( 'NONE',  ( 2.764680872515351773, 11.36963888406687317, 9.232963481057801403 ) ) ;
#5998=EDGE_CURVE ( 'NONE', #12499, #393, #6910, .T. ) ;
#6001=LINE ( 'NONE', #15167, #7848 ) ;
#6010=ORIENTED_EDGE ( 'NONE', *, *, #12351, .F. ) ;
#6011=CARTESIAN_POINT ( 'NONE',  ( 0.000000000000000000, 13.40591150984237245, -7.739906618939567551 ) ) ;
#6012=CARTESIAN_POINT ( 'NONE',  ( 0.2818303916520938368, -15.25429862889478194, -5.259531939870360162 ) ) ;
#6026=CARTESIAN_POINT ( 'NONE',  ( 0.07473579423048559711, 2.569134216959106265, -15.04916547791951764 ) ) ;
#6028=CARTESIAN_POINT ( 'NONE',  ( 0.007349505829628596824, -13.44926448535269792, 5.204557061642240079 ) ) ;
#6030=VERTEX_POINT ( 'NONE', #3140 ) ;
#6031=ORIENTED_EDGE ( 'NONE', *, *, #6307, .F. ) ;
#6036=CARTESIAN_POINT ( 'NONE',  ( 1.749999999999999778, 0.000000000000000000, 0.000000000000000000 ) ) ;
#6041=AXIS2_PLACEMENT_3D ( 'NONE', #8743, #12285, #1759 ) ;
#6046=DIRECTION ( 'NONE',  ( -1.000000000000000000, -0.000000000000000000, -0.000000000000000000 ) ) ;
#6050=TOROIDAL_SURFACE ( 'NONE', #13650, 14.01039946648073986, 8.000000000000000000 ) ;
#6052=CARTESIAN_POINT ( 'NONE',  ( 0.2076372544708497692, 10.30022894898806207, 12.04200105039474167 ) ) ;
#6056=CARTESIAN_POINT ( 'NONE',  ( 0.1920564340659374758, 5.295083827234713603, 14.93837896275551813 ) ) ;
#6066=DIRECTION ( 'NONE',  ( -1.000000000000000000, -0.000000000000000000, -0.000000000000000000 ) ) ;
#6070=ADVANCED_FACE ( 'NONE', ( #11498, #5301 ), #2978, .F. ) ;
#6075=CARTESIAN_POINT ( 'NONE',  ( 1.039999999999998925, -17.29145405592692342, 4.835383649608409939 ) ) ;
#6099=CARTESIAN_POINT ( 'NONE',  ( 1.394999999999999574, 4.835383649608472112, 17.29145405592690565 ) ) ;
#6100=CARTESIAN_POINT ( 'NONE',  ( 2.697960337741387438, -15.03709480088670070, -2.583706482362191359 ) ) ;
#6101=EDGE_CURVE ( 'NONE', #11883, #5435, #6167, .T. ) ;
#6112=ORIENTED_EDGE ( 'NONE', *, *, #9224, .F. ) ;
#6119=CIRCLE ( 'NONE', #5404, 2.524999999999999467 ) ;
#6122=CARTESIAN_POINT ( 'NONE',  ( 2.010451917295051238, -5.008579424861679286, 16.73367785739755575 ) ) ;
#6123=CARTESIAN_POINT ( 'NONE',  ( 0.02531912748679520167, -11.36963888406680923, -9.232963481057881339 ) ) ;
#6128=ORIENTED_EDGE ( 'NONE', *, *, #4859, .F. ) ;
#6130=CARTESIAN_POINT ( 'NONE',  ( 0.008751532932800723183, 13.40591150984233870, -5.214906618939568084 ) ) ;
#6133=CARTESIAN_POINT ( 'NONE',  ( 2.697960371751379149, 9.756102650610401383, -11.73065272960052496 ) ) ;
#6138=CARTESIAN_POINT ( 'NONE',  ( 2.789999999999999147, -13.68080036884344963, -5.229914364928496262 ) ) ;
#6142=DIRECTION ( 'NONE',  ( 1.000000000000000000, -0.000000000000000000, 0.000000000000000000 ) ) ;
#6146=CARTESIAN_POINT ( 'NONE',  ( 0.09203962824861877667, -11.73065272960070260, 9.756102650610195326 ) ) ;
#6160=EDGE_LOOP ( 'NONE', ( #3169, #9891, #14751, #13572, #6628, #11910 ) ) ;
#6167=B_SPLINE_CURVE_WITH_KNOTS ( 'NONE', 3,
 ( #7118, #5826, #2435, #8048, #12946, #3657, #13882, #12722 ),
 .UNSPECIFIED., .F., .F.,
 ( 4, 2, 2, 4 ),
 ( 2.154797737777091420E-07, 0.001895231411415143749, 0.002842739377235822817, 0.003790247343056503404 ),
 .UNSPECIFIED. ) ;
#6169=ADVANCED_FACE ( 'NONE', ( #6892 ), #15208, .F. ) ;
#6171=EDGE_CURVE ( 'NONE', #13716, #13491, #8121, .T. ) ;
#6172=LINE ( 'NONE', #6099, #3078 ) ;
#6173=CARTESIAN_POINT ( 'NONE',  ( 1.749999999999999778, -17.39253030560838198, -4.458161950358684678 ) ) ;
#6179=CARTESIAN_POINT ( 'NONE',  ( 1.749999999999999778, 0.000000000000000000, 0.000000000000000000 ) ) ;
#6181=ORIENTED_EDGE ( 'NONE', *, *, #13306, .F. ) ;
#6185=EDGE_CURVE ( 'NONE', #484, #3683, #486, .T. ) ;
#6187=DIRECTION ( 'NONE',  ( 0.000000000000000000, 0.000000000000000000, 1.000000000000000000 ) ) ;
#6188=DIRECTION ( 'NONE',  ( 0.000000000000000000, 0.000000000000000000, 1.000000000000000000 ) ) ;
#6189=LINE ( 'NONE', #11235, #6357 ) ;
#6201=ORIENTED_EDGE ( 'NONE', *, *, #8319, .T. ) ;
#6206=DIRECTION ( 'NONE',  ( -1.000000000000000000, -0.000000000000000000, -0.000000000000000000 ) ) ;
#6211=VERTEX_POINT ( 'NONE', #489 ) ;
#6212=DIRECTION ( 'NONE',  ( -1.000000000000000000, -0.000000000000000000, 0.000000000000000000 ) ) ;
#6216=DIRECTION ( 'NONE',  ( -1.000000000000000000, -0.000000000000000000, -0.000000000000000000 ) ) ;
#6217=CARTESIAN_POINT ( 'NONE',  ( -5.209999999999999964, 0.000000000000000000, 0.000000000000000000 ) ) ;
#6219=CARTESIAN_POINT ( 'NONE',  ( 2.597943646031741771, 15.58455734132147974, -2.883512197588947501 ) ) ;
#6220=DIRECTION ( 'NONE',  ( -1.000000000000000000, 0.000000000000000000, 0.000000000000000000 ) ) ;
#6222=VERTEX_POINT ( 'NONE', #14265 ) ;
#6223=VERTEX_POINT ( 'NONE', #258 ) ;
#6227=CARTESIAN_POINT ( 'NONE',  ( 0.02531912748605881155, 13.68080036884355621, -5.229914364928207604 ) ) ;
#6229=ORIENTED_EDGE ( 'NONE', *, *, #3001, .T. ) ;
#6231=EDGE_LOOP ( 'NONE', ( #6128, #1231, #10736, #8232, #465, #5077 ) ) ;
#6236=ORIENTED_EDGE ( 'NONE', *, *, #5417, .F. ) ;
#6237=CIRCLE ( 'NONE', #2311, 17.95481323787947403 ) ;
#6246=FACE_OUTER_BOUND ( 'NONE', #5925, .T. ) ;
#6247=VECTOR ( 'NONE', #14916, 1000.000000000000000 ) ;
#6254=ORIENTED_EDGE ( 'NONE', *, *, #7210, .F. ) ;
#6257=LINE ( 'NONE', #8702, #2085 ) ;
#6277=ORIENTED_EDGE ( 'NONE', *, *, #1503, .F. ) ;
#6281=CARTESIAN_POINT ( 'NONE',  ( 2.789999999999999147, 14.19996452731189152, 4.595504208220079434 ) ) ;
#6284=AXIS2_PLACEMENT_3D ( 'NONE', #2921, #5312, #7610 ) ;
#6286=DIRECTION ( 'NONE',  ( 0.000000000000000000, 0.000000000000000000, 1.000000000000000000 ) ) ;
#6292=CARTESIAN_POINT ( 'NONE',  ( 2.764680872515354437, 13.68080036884355621, -5.229914364928207604 ) ) ;
#6295=CIRCLE ( 'NONE', #12172, 14.01039946648073986 ) ;
#6304=DIRECTION ( 'NONE',  ( 0.000000000000000000, 2.061057595219969177E-15, -1.000000000000000000 ) ) ;
#6306=CARTESIAN_POINT ( 'NONE',  ( 2.789999999999999147, 0.000000000000000000, 0.000000000000000000 ) ) ;
#6307=EDGE_CURVE ( 'NONE', #7052, #11075, #3831, .T. ) ;
#6310=EDGE_LOOP ( 'NONE', ( #4964, #884, #13160, #8922, #12785, #12298 ) ) ;
#6319=ORIENTED_EDGE ( 'NONE', *, *, #13904, .F. ) ;
#6329=CIRCLE ( 'NONE', #13449, 17.95481323787947403 ) ;
#6334=VERTEX_POINT ( 'NONE', #798 ) ;
#6336=DIRECTION ( 'NONE',  ( -1.000000000000000000, 0.000000000000000000, 0.000000000000000000 ) ) ;
#6342=CARTESIAN_POINT ( 'NONE',  ( 2.789999999999999147, -8.624777288397723396, -11.04103753892280615 ) ) ;
#6350=ORIENTED_EDGE ( 'NONE', *, *, #46, .T. ) ;
#6351=VERTEX_POINT ( 'NONE', #11257 ) ;
#6352=EDGE_CURVE ( 'NONE', #1772, #2383, #5860, .T. ) ;
#6357=VECTOR ( 'NONE', #4178, 1000.000000000000000 ) ;
#6358=DIRECTION ( 'NONE',  ( 1.000000000000000000, 0.000000000000000000, 0.000000000000000000 ) ) ;
#6365=EDGE_CURVE ( 'NONE', #7999, #1061, #327, .T. ) ;
#6370=CIRCLE ( 'NONE', #4174, 2.524999999999999023 ) ;
#6372=VERTEX_POINT ( 'NONE', #7650 ) ;
#6382=AXIS2_PLACEMENT_3D ( 'NONE', #11278, #10278, #10054 ) ;
#6383=DIRECTION ( 'NONE',  ( -1.000000000000000000, 0.000000000000000000, -0.000000000000000000 ) ) ;
#6386=EDGE_CURVE ( 'NONE', #9357, #6351, #1733, .T. ) ;
#6392=( NAMED_UNIT ( * ) SI_UNIT ( $, .STERADIAN. ) SOLID_ANGLE_UNIT ( ) );
#6393=ORIENTED_EDGE ( 'NONE', *, *, #7511, .F. ) ;
#6395=ORIENTED_EDGE ( 'NONE', *, *, #8150, .T. ) ;
#6400=DIRECTION ( 'NONE',  ( -1.000000000000000000, -0.000000000000000000, -0.000000000000000000 ) ) ;
#6401=ORIENTED_EDGE ( 'NONE', *, *, #3084, .F. ) ;
#6404=CARTESIAN_POINT ( 'NONE',  ( 0.1438988480159978933, 14.59528211758547478, 5.279841123860917307 ) ) ;
#6417=ORIENTED_EDGE ( 'NONE', *, *, #6671, .T. ) ;
#6419=DIRECTION ( 'NONE',  ( 0.000000000000000000, 0.000000000000000000, 1.000000000000000000 ) ) ;
#6430=CYLINDRICAL_SURFACE ( 'NONE', #13365, 8.400000000000000355 ) ;
#6440=EDGE_CURVE ( 'NONE', #5814, #12657, #7723, .T. ) ;
#6451=AXIS2_PLACEMENT_3D ( 'NONE', #5223, #3745, #13109 ) ;
#6455=CARTESIAN_POINT ( 'NONE',  ( 2.764680872515353993, -5.229914364928256454, -13.68080036884353845 ) ) ;
#6456=DIRECTION ( 'NONE',  ( -1.000000000000000000, -0.000000000000000000, -0.000000000000000000 ) ) ;
#6459=CARTESIAN_POINT ( 'NONE',  ( -5.209999999999999964, 0.000000000000000000, 0.000000000000000000 ) ) ;
#6464=ORIENTED_EDGE ( 'NONE', *, *, #10555, .F. ) ;
#6471=ORIENTED_EDGE ( 'NONE', *, *, #13221, .T. ) ;
#6472=DIRECTION ( 'NONE',  ( -1.000000000000000000, -0.000000000000000000, 0.000000000000000000 ) ) ;
#6475=CARTESIAN_POINT ( 'NONE',  ( 2.789999999999999147, -4.595504208219929332, -14.19996452731193948 ) ) ;
#6480=ORIENTED_EDGE ( 'NONE', *, *, #7879, .T. ) ;
#6482=CARTESIAN_POINT ( 'NONE',  ( -6.158890435332099336E-14, 13.21862218141514234, 5.211197193340741940 ) ) ;
#6484=ORIENTED_EDGE ( 'NONE', *, *, #5526, .F. ) ;
#6486=CARTESIAN_POINT ( 'NONE',  ( 2.021362740937213687, -5.021526291670196152, -16.74220655292943505 ) ) ;
#6491=AXIS2_PLACEMENT_3D ( 'NONE', #11366, #6532, #9143 ) ;
#6495=ORIENTED_EDGE ( 'NONE', *, *, #12546, .T. ) ;
#6500=ORIENTED_EDGE ( 'NONE', *, *, #14660, .T. ) ;
#6511=CARTESIAN_POINT ( 'NONE',  ( 0.5537796877189864464, -11.41743294611084103, 12.52687487503415298 ) ) ;
#6517=AXIS2_PLACEMENT_3D ( 'NONE', #10325, #12837, #2096 ) ;
#6518=CARTESIAN_POINT ( 'NONE',  ( 1.039999999999996927, 4.835383649608473000, 17.29145405592690565 ) ) ;
#6522=ORIENTED_EDGE ( 'NONE', *, *, #5365, .F. ) ;
#6525=CYLINDRICAL_SURFACE ( 'NONE', #5797, 8.400000000000000355 ) ;
#6532=DIRECTION ( 'NONE',  ( -1.000000000000000000, -0.000000000000000000, -0.000000000000000000 ) ) ;
#6535=ORIENTED_EDGE ( 'NONE', *, *, #6578, .F. ) ;
#6536=VECTOR ( 'NONE', #6142, 1000.000000000000000 ) ;
#6544=VERTEX_POINT ( 'NONE', #1032 ) ;
#6546=CARTESIAN_POINT ( 'NONE',  ( 2.790000000000060876, -14.05326139264726137, -2.096282088614914940 ) ) ;
#6548=EDGE_CURVE ( 'NONE', #3069, #5814, #12062, .T. ) ;
#6550=B_SPLINE_CURVE_WITH_KNOTS ( 'NONE', 3,
 ( #10795, #9633, #1495, #8561, #14327, #13168, #2654, #7347 ),
 .UNSPECIFIED., .F., .F.,
 ( 4, 2, 2, 4 ),
 ( 2.445728210282191027E-07, 0.001895260649874687875, 0.002842768688401520541, 0.003790276726928352991 ),
 .UNSPECIFIED. ) ;
#6555=ORIENTED_EDGE ( 'NONE', *, *, #5548, .F. ) ;
#6558=EDGE_CURVE ( 'NONE', #10985, #12627, #11481, .T. ) ;
#6565=CARTESIAN_POINT ( 'NONE',  ( 1.749999999999999778, 4.835383649608472112, 17.29145405592690210 ) ) ;
#6566=CARTESIAN_POINT ( 'NONE',  ( 2.021362784118868827, -12.71987259277426574, -11.98841295390611528 ) ) ;
#6573=EDGE_CURVE ( 'NONE', #1400, #6211, #10535, .T. ) ;
#6578=EDGE_CURVE ( 'NONE', #4401, #12582, #3177, .T. ) ;
#6580=DIRECTION ( 'NONE',  ( -1.000000000000000000, -0.000000000000000000, -0.000000000000000000 ) ) ;
#6583=AXIS2_PLACEMENT_3D ( 'NONE', #1952, #8781, #783 ) ;
#6597=B_SPLINE_CURVE_WITH_KNOTS ( 'NONE', 3,
 ( #1119, #13958, #10722, #10501 ),
 .UNSPECIFIED., .F., .F.,
 ( 4, 4 ),
 ( 0.005123695899043910658, 0.005814329666474868374 ),
 .UNSPECIFIED. ) ;
#6608=CARTESIAN_POINT ( 'NONE',  ( 2.789999999999999147, -11.07980565117273386, -9.999777909380050289 ) ) ;
#6620=DIRECTION ( 'NONE',  ( -1.000000000000000000, 0.000000000000000000, 0.000000000000000000 ) ) ;
#6621=CIRCLE ( 'NONE', #12244, 17.95481323787947758 ) ;
#6623=VERTEX_POINT ( 'NONE', #2643 ) ;
#6628=ORIENTED_EDGE ( 'NONE', *, *, #3464, .F. ) ;
#6631=CARTESIAN_POINT ( 'NONE',  ( 2.715264245299034318, -11.74839219818094982, 9.749517823373967218 ) ) ;
#6636=CARTESIAN_POINT ( 'NONE',  ( 2.787319300893938756, -13.26676317347970091, -5.214906618939852301 ) ) ;
#6643=EDGE_LOOP ( 'NONE', ( #6319, #2795, #10227, #9099 ) ) ;
#6646=VERTEX_POINT ( 'NONE', #395 ) ;
#6652=VERTEX_POINT ( 'NONE', #3952 ) ;
#6669=CARTESIAN_POINT ( 'NONE',  ( 1.039999999999997815, -12.55714665599996316, 12.83329210556827604 ) ) ;
#6671=EDGE_CURVE ( 'NONE', #12582, #13265, #4389, .T. ) ;
#6673=CYLINDRICAL_SURFACE ( 'NONE', #945, 2.524999999999999467 ) ;
#6675=CARTESIAN_POINT ( 'NONE',  ( 2.789999999999999147, -5.229914364928256454, -13.68080036884353845 ) ) ;
#6677=CARTESIAN_POINT ( 'NONE',  ( 0.000000000000000000, 13.40591150984226587, 7.739906618939754956 ) ) ;
#6679=VERTEX_POINT ( 'NONE', #3636 ) ;
#6685=FACE_OUTER_BOUND ( 'NONE', #2765, .T. ) ;
#6689=FACE_OUTER_BOUND ( 'NONE', #9399, .T. ) ;
#6699=DIRECTION ( 'NONE',  ( 0.000000000000000000, 0.000000000000000000, 1.000000000000000000 ) ) ;
#6700=ADVANCED_FACE ( 'NONE', ( #6246 ), #13442, .T. ) ;
#6702=ORIENTED_EDGE ( 'NONE', *, *, #14364, .F. ) ;
#6705=DIRECTION ( 'NONE',  ( 0.000000000000000000, 0.000000000000000000, -1.000000000000000000 ) ) ;
#6708=ORIENTED_EDGE ( 'NONE', *, *, #5365, .T. ) ;
#6720=DIRECTION ( 'NONE',  ( 0.000000000000000000, 0.000000000000000000, -1.000000000000000000 ) ) ;
#6729=CARTESIAN_POINT ( 'NONE',  ( -6.225199705999128148E-14, 2.096282088614769279, 14.05326139264728624 ) ) ;
#6732=AXIS2_PLACEMENT_3D ( 'NONE', #1639, #13157, #11922 ) ;
#6741=ORIENTED_EDGE ( 'NONE', *, *, #6573, .F. ) ;
#6764=EDGE_CURVE ( 'NONE', #11452, #4926, #8294, .T. ) ;
#6766=ORIENTED_EDGE ( 'NONE', *, *, #8614, .T. ) ;
#6770=VERTEX_POINT ( 'NONE', #7787 ) ;
#6771=AXIS2_PLACEMENT_3D ( 'NONE', #2781, #544, #5257 ) ;
#6779=DIRECTION ( 'NONE',  ( 0.000000000000000000, 0.000000000000000000, 1.000000000000000000 ) ) ;
#6780=CIRCLE ( 'NONE', #8476, 14.01039946648073986 ) ;
#6786=CARTESIAN_POINT ( 'NONE',  ( -10.00000000000000000, 0.000000000000000000, 0.000000000000000000 ) ) ;
#6787=CIRCLE ( 'NONE', #13151, 2.524999999999998579 ) ;
#6792=AXIS2_PLACEMENT_3D ( 'NONE', #10408, #87, #13004 ) ;
#6796=AXIS2_PLACEMENT_3D ( 'NONE', #9877, #14509, #12099 ) ;
#6798=ADVANCED_FACE ( 'NONE', ( #14784 ), #13620, .F. ) ;
#6815=CARTESIAN_POINT ( 'NONE',  ( -5.209999999999999964, 0.000000000000000000, 0.000000000000000000 ) ) ;
#6818=ORIENTED_EDGE ( 'NONE', *, *, #9986, .F. ) ;
#6825=DIRECTION ( 'NONE',  ( 0.000000000000000000, 0.000000000000000000, 1.000000000000000000 ) ) ;
#6834=CARTESIAN_POINT ( 'NONE',  ( 2.337784062669524321, -16.32199768300081288, 3.429166897524368984 ) ) ;
#6838=EDGE_CURVE ( 'NONE', #9357, #11164, #9037, .T. ) ;
#6841=CYLINDRICAL_SURFACE ( 'NONE', #4493, 2.524999999999999467 ) ;
#6843=CARTESIAN_POINT ( 'NONE',  ( 2.697960337741387438, 15.03709480088671846, 2.583706482362086110 ) ) ;
#6849=ORIENTED_EDGE ( 'NONE', *, *, #10644, .F. ) ;
#6851=ORIENTED_EDGE ( 'NONE', *, *, #11681, .F. ) ;
#6852=EDGE_CURVE ( 'NONE', #12499, #10760, #7635, .T. ) ;
#6857=TOROIDAL_SURFACE ( 'NONE', #10534, 14.01039946648073986, 8.000000000000000000 ) ;
#6860=CARTESIAN_POINT ( 'NONE',  ( 1.039999999999997593, 0.000000000000000000, 0.000000000000000000 ) ) ;
#6870=VERTEX_POINT ( 'NONE', #11539 ) ;
#6871=EDGE_LOOP ( 'NONE', ( #7456, #4452, #2495, #7808 ) ) ;
#6878=CARTESIAN_POINT ( 'NONE',  ( 8.000000000000000000, 0.000000000000000000, 0.000000000000000000 ) ) ;
#6882=FACE_OUTER_BOUND ( 'NONE', #9329, .T. ) ;
#6884=ORIENTED_EDGE ( 'NONE', *, *, #12938, .F. ) ;
#6885=CARTESIAN_POINT ( 'NONE',  ( 1.039999999999997593, 0.000000000000000000, 0.000000000000000000 ) ) ;
#6892=FACE_OUTER_BOUND ( 'NONE', #14761, .T. ) ;
#6895=DIRECTION ( 'NONE',  ( -1.000000000000000000, -0.000000000000000000, -0.000000000000000000 ) ) ;
#6896=CARTESIAN_POINT ( 'NONE',  ( 2.789999999999999147, 11.07980565117280314, 9.999777909379972129 ) ) ;
#6904=CARTESIAN_POINT ( 'NONE',  ( 1.039999999999997593, 4.835383649608715473, -17.29145405592683815 ) ) ;
#6905=DIRECTION ( 'NONE',  ( 0.000000000000000000, 0.000000000000000000, 1.000000000000000000 ) ) ;
#6907=ORIENTED_EDGE ( 'NONE', *, *, #14063, .T. ) ;
#6908=CARTESIAN_POINT ( 'NONE',  ( 2.236220346785029456, -16.55730827443882447, 3.624349476775136303 ) ) ;
#6909=DIRECTION ( 'NONE',  ( -1.000000000000000000, -0.000000000000000000, -0.000000000000000000 ) ) ;
#6910=B_SPLINE_CURVE_WITH_KNOTS ( 'NONE', 3,
 ( #8965, #11347, #12576, #11416 ),
 .UNSPECIFIED., .F., .F.,
 ( 4, 4 ),
 ( 0.0002742066915197750193, 0.0006916721208754025157 ),
 .UNSPECIFIED. ) ;
#6918=CARTESIAN_POINT ( 'NONE',  ( 0.000000000000000000, 8.624777288397805108, 11.04103753892274575 ) ) ;
#6921=EDGE_CURVE ( 'NONE', #12007, #6623, #173, .T. ) ;
#6923=ORIENTED_EDGE ( 'NONE', *, *, #7707, .F. ) ;
#6928=CARTESIAN_POINT ( 'NONE',  ( 0.2076372544708503520, -10.30022894898797858, -12.04200105039481095 ) ) ;
#6936=CARTESIAN_POINT ( 'NONE',  ( 0.7686372430964468760, 17.00993931356758537, -4.022333916463615822 ) ) ;
#6937=EDGE_CURVE ( 'NONE', #5435, #11802, #3750, .T. ) ;
#6948=DIRECTION ( 'NONE',  ( 0.000000000000000000, 0.000000000000000000, 1.000000000000000000 ) ) ;
#6955=VERTEX_POINT ( 'NONE', #15087 ) ;
#6962=CARTESIAN_POINT ( 'NONE',  ( 50.00050000000000239, 0.000000000000000000, 4.000000000000000000 ) ) ;
#6971=CARTESIAN_POINT ( 'NONE',  ( 0.02531912748606228100, -13.68080036884352246, 5.229914364928304416 ) ) ;
#6972=CARTESIAN_POINT ( 'NONE',  ( 1.885839510111769313, -17.01651022436359995, -4.928563447326470559 ) ) ;
#6988=CIRCLE ( 'NONE', #6491, 17.95481323787947758 ) ;
#6991=ADVANCED_FACE ( 'NONE', ( #7214 ), #1368, .F. ) ;
#6992=ORIENTED_EDGE ( 'NONE', *, *, #12540, .T. ) ;
#6995=ORIENTED_EDGE ( 'NONE', *, *, #4425, .F. ) ;
#6999=VECTOR ( 'NONE', #12464, 1000.000000000000000 ) ;
#7002=CARTESIAN_POINT ( 'NONE',  ( 0.09203966225861190398, -2.583706482361930235, -15.03709480088674688 ) ) ;
#7011=B_SPLINE_CURVE_WITH_KNOTS ( 'NONE', 3,
 ( #8241, #11776, #5945, #10629 ),
 .UNSPECIFIED., .F., .F.,
 ( 4, 4 ),
 ( 0.005123713096549380695, 0.005814346476695810180 ),
 .UNSPECIFIED. ) ;
#7013=EDGE_LOOP ( 'NONE', ( #8876, #14198, #9917, #15186, #10510, #11036, #1553, #10137, #11775, #4848, #4002, #10040, #4986, #369, #3815, #195, #8844, #5411, #4319, #9466, #13353, #213, #9325, #6849, #4569, #3411, #15047 ) ) ;
#7018=CARTESIAN_POINT ( 'NONE',  ( 2.740003281797976253, 13.99876742897266446, -5.264737421541377138 ) ) ;
#7024=AXIS2_PLACEMENT_3D ( 'NONE', #6677, #4225, #5533 ) ;
#7039=DIRECTION ( 'NONE',  ( -1.000000000000000000, -0.000000000000000000, -0.000000000000000000 ) ) ;
#7047=CARTESIAN_POINT ( 'NONE',  ( 2.789999999999999147, 12.98979500319701508, -5.249430348645618416 ) ) ;
#7050=CIRCLE ( 'NONE', #13678, 2.524999999999999023 ) ;
#7052=VERTEX_POINT ( 'NONE', #2911 ) ;
#7053=CARTESIAN_POINT ( 'NONE',  ( 2.010451917295053459, -16.73367785739753444, -5.008579424861741458 ) ) ;
#7056=CARTESIAN_POINT ( 'NONE',  ( 1.885839528871395609, 12.77651625388916301, -12.27244837507599762 ) ) ;
#7060=CARTESIAN_POINT ( 'NONE',  ( 1.394999999999999574, -12.55714665599978019, -12.83329210556845013 ) ) ;
#7061=FACE_OUTER_BOUND ( 'NONE', #2031, .T. ) ;
#7076=CARTESIAN_POINT ( 'NONE',  ( 0.2291144030788790364, -15.06658931286050951, 5.279841123860816055 ) ) ;
#7077=CARTESIAN_POINT ( 'NONE',  ( 0.9041604898882319441, -4.928563447326170355, -17.01651022436368876 ) ) ;
#7090=DIRECTION ( 'NONE',  ( -1.000000000000000000, -0.000000000000000000, -0.000000000000000000 ) ) ;
#7093=ORIENTED_EDGE ( 'NONE', *, *, #12295, .T. ) ;
#7104=CARTESIAN_POINT ( 'NONE',  ( 2.135044773435426091, -16.44225436089929815, 5.086950209440439075 ) ) ;
#7108=ORIENTED_EDGE ( 'NONE', *, *, #13691, .T. ) ;
#7113=CIRCLE ( 'NONE', #1348, 14.01039946648074341 ) ;
#7118=CARTESIAN_POINT ( 'NONE',  ( 2.764680872513688659, 2.311161484776556030, 14.46287784598618309 ) ) ;
#7130=EDGE_LOOP ( 'NONE', ( #4402, #12637, #13898, #13580 ) ) ;
#7131=B_SPLINE_CURVE_WITH_KNOTS ( 'NONE', 3,
 ( #2309, #1164, #11170, #9944 ),
 .UNSPECIFIED., .F., .F.,
 ( 4, 4 ),
 ( 1.988537749986029444E-07, 0.0006916721208753980705 ),
 .UNSPECIFIED. ) ;
#7133=CARTESIAN_POINT ( 'NONE',  ( 2.790000000000000924, 4.898587196589412829E-16, -4.000000000000000000 ) ) ;
#7134=CARTESIAN_POINT ( 'NONE',  ( 1.039999999999998925, -17.29145405592692342, 4.835383649608409939 ) ) ;
#7135=CARTESIAN_POINT ( 'NONE',  ( 2.021362784118871936, 11.98841295390615613, -12.71987259277422844 ) ) ;
#7142=ORIENTED_EDGE ( 'NONE', *, *, #14651, .T. ) ;
#7151=VERTEX_POINT ( 'NONE', #14592 ) ;
#7152=CARTESIAN_POINT ( 'NONE',  ( 0.3493891680732006955, -15.53033051714692547, 5.240368680323494566 ) ) ;
#7157=B_SPLINE_CURVE_WITH_KNOTS ( 'NONE', 3,
 ( #5055, #11944, #1736, #1660, #563, #6122, #1433, #2739 ),
 .UNSPECIFIED., .F., .F.,
 ( 4, 2, 2, 4 ),
 ( 1.984117563342667082E-07, 0.001895214258086352519, 0.002842722181251361793, 0.003790230104416370850 ),
 .UNSPECIFIED. ) ;
#7158=CARTESIAN_POINT ( 'NONE',  ( 0.7686372430964689695, -4.022333916463475489, -17.00993931356764932 ) ) ;
#7159=ORIENTED_EDGE ( 'NONE', *, *, #5267, .T. ) ;
#7166=VERTEX_POINT ( 'NONE', #3060 ) ;
#7171=CYLINDRICAL_SURFACE ( 'NONE', #2570, 8.400000000000000355 ) ;
#7180=CARTESIAN_POINT ( 'NONE',  ( 2.789999999999999147, 1.621424371464993087E-13, -12.95481323787947936 ) ) ;
#7191=ADVANCED_FACE ( 'NONE', ( #14898 ), #9129, .F. ) ;
#7197=ORIENTED_EDGE ( 'NONE', *, *, #1768, .T. ) ;
#7201=CARTESIAN_POINT ( 'NONE',  ( 2.715264245299032986, 11.74839219818101910, -9.749517823373880177 ) ) ;
#7203=CARTESIAN_POINT ( 'NONE',  ( 2.789999999999999147, -13.40591150984221080, -5.214906618939850524 ) ) ;
#7210=EDGE_CURVE ( 'NONE', #10832, #8536, #8089, .T. ) ;
#7211=ADVANCED_FACE ( 'NONE', ( #1989 ), #6673, .F. ) ;
#7214=FACE_OUTER_BOUND ( 'NONE', #6160, .T. ) ;
#7217=DIRECTION ( 'NONE',  ( 0.000000000000000000, 0.000000000000000000, 1.000000000000000000 ) ) ;
#7221=ORIENTED_EDGE ( 'NONE', *, *, #8336, .T. ) ;
#7224=CARTESIAN_POINT ( 'NONE',  ( 0.1438988480186108865, -14.59528211759996630, 5.279841123860814278 ) ) ;
#7226=CARTESIAN_POINT ( 'NONE',  ( 2.789999999999999147, 13.87420763704361093, -1.948757464274220697 ) ) ;
#7230=EDGE_CURVE ( 'NONE', #2043, #4505, #3283, .T. ) ;
#7231=CARTESIAN_POINT ( 'NONE',  ( 0.07473579423048611059, -2.569134216959001904, 15.04916547791953541 ) ) ;
#7238=ADVANCED_FACE ( 'NONE', ( #3360 ), #4889, .T. ) ;
#7245=ORIENTED_EDGE ( 'NONE', *, *, #2735, .F. ) ;
#7246=CARTESIAN_POINT ( 'NONE',  ( 0.000000000000000000, -11.04103753892265871, -8.624777288397922348 ) ) ;
#7257=CARTESIAN_POINT ( 'NONE',  ( 0.7686372158811279887, 12.71987259277452154, -11.98841295390584705 ) ) ;
#7262=ORIENTED_EDGE ( 'NONE', *, *, #1654, .F. ) ;
#7268=DIRECTION ( 'NONE',  ( 1.000000000000000000, 0.000000000000000000, 0.000000000000000000 ) ) ;
#7274=DIRECTION ( 'NONE',  ( 0.000000000000000000, 0.000000000000000000, 1.000000000000000000 ) ) ;
#7286=DIRECTION ( 'NONE',  ( -1.000000000000000000, 0.000000000000000000, -0.000000000000000000 ) ) ;
#7292=CARTESIAN_POINT ( 'NONE',  ( 0.1438988480159978933, 14.59528211758547478, 5.279841123860917307 ) ) ;
#7295=AXIS2_PLACEMENT_3D ( 'NONE', #7363, #10808, #263 ) ;
#7297=EDGE_CURVE ( 'NONE', #2515, #10827, #11723, .T. ) ;
#7299=VERTEX_POINT ( 'NONE', #9500 ) ;
#7302=CARTESIAN_POINT ( 'NONE',  ( 2.764680872515351329, 14.46287784598617421, -2.311161484776606212 ) ) ;
#7309=CARTESIAN_POINT ( 'NONE',  ( 0.02531912748606271468, -5.229914364928256454, -13.68080036884353845 ) ) ;
#7314=CARTESIAN_POINT ( 'NONE',  ( -10.00000000000000000, 0.000000000000000000, 0.000000000000000000 ) ) ;
#7319=AXIS2_PLACEMENT_3D ( 'NONE', #1673, #6358, #11041 ) ;
#7345=CARTESIAN_POINT ( 'NONE',  ( 2.790000000000000036, 0.000000000000000000, 0.000000000000000000 ) ) ;
#7347=CARTESIAN_POINT ( 'NONE',  ( 1.039999999999996261, 12.83329210556831512, 12.55714665599991697 ) ) ;
#7353=CARTESIAN_POINT ( 'NONE',  ( 0.000000000000000000, 0.000000000000000000, 0.000000000000000000 ) ) ;
#7357=AXIS2_PLACEMENT_3D ( 'NONE', #4143, #3054, #4365 ) ;
#7363=CARTESIAN_POINT ( 'NONE',  ( 0.000000000000000000, 15.47981323787947794, 0.000000000000000000 ) ) ;
#7366=ORIENTED_EDGE ( 'NONE', *, *, #2598, .T. ) ;
#7386=CARTESIAN_POINT ( 'NONE',  ( 0.000000000000000000, 12.98979500319701685, -5.249430348645618416 ) ) ;
#7394=CARTESIAN_POINT ( 'NONE',  ( 2.789999999999999147, -5.249430348645846678, 12.98979500319692448 ) ) ;
#7395=CARTESIAN_POINT ( 'NONE',  ( 2.740003288479520904, -2.439987328297072544, 14.75565684666126387 ) ) ;
#7402=CYLINDRICAL_SURFACE ( 'NONE', #11660, 17.95481323787947403 ) ;
#7415=CARTESIAN_POINT ( 'NONE',  ( 2.789999999999999147, -15.47981323787947794, -1.080949580976661932E-13 ) ) ;
#7418=CARTESIAN_POINT ( 'NONE',  ( 2.790000000000000924, 0.000000000000000000, 0.000000000000000000 ) ) ;
#7419=CARTESIAN_POINT ( 'NONE',  ( 1.749999999999999778, -17.29145405592685236, -4.835383649608663070 ) ) ;
#7420=ORIENTED_EDGE ( 'NONE', *, *, #660, .F. ) ;
#7424=B_SPLINE_CURVE_WITH_KNOTS ( 'NONE', 3,
 ( #14413, #9291, #3442, #12803 ),
 .UNSPECIFIED., .F., .F.,
 ( 4, 4 ),
 ( 1.984117563342612819E-07, 0.0009182716802119580664 ),
 .UNSPECIFIED. ) ;
#7425=EDGE_CURVE ( 'NONE', #3101, #9188, #5135, .T. ) ;
#7427=B_SPLINE_CURVE_WITH_KNOTS ( 'NONE', 3,
 ( #11830, #63, #9381, #3765, #4863, #8450, #2623, #1306 ),
 .UNSPECIFIED., .F., .F.,
 ( 4, 2, 2, 4 ),
 ( 4.663089536307126026E-07, 0.001898630414085407782, 0.002847712466651296237, 0.003796794519217184909 ),
 .UNSPECIFIED. ) ;
#7443=CARTESIAN_POINT ( 'NONE',  ( 1.749999999999999778, 17.29145405592688789, 4.835383649608534284 ) ) ;
#7456=ORIENTED_EDGE ( 'NONE', *, *, #540, .T. ) ;
#7463=B_SPLINE_CURVE_WITH_KNOTS ( 'NONE', 3,
 ( #4739, #182, #9571, #1340 ),
 .UNSPECIFIED., .F., .F.,
 ( 4, 4 ),
 ( 2.159563976394568454E-07, 0.0006916893629248619269 ),
 .UNSPECIFIED. ) ;
#7473=AXIS2_PLACEMENT_3D ( 'NONE', #9462, #7, #4947 ) ;
#7485=VECTOR ( 'NONE', #12162, 1000.000000000000000 ) ;
#7490=ORIENTED_EDGE ( 'NONE', *, *, #9634, .F. ) ;
#7492=LINE ( 'NONE', #2875, #7485 ) ;
#7498=DIRECTION ( 'NONE',  ( 0.000000000000000000, 0.000000000000000000, 1.000000000000000000 ) ) ;
#7505=LINE ( 'NONE', #12260, #13463 ) ;
#7506=CARTESIAN_POINT ( 'NONE',  ( 0.000000000000000000, 1.621424371464993087E-13, -15.47981323787947794 ) ) ;
#7507=DIRECTION ( 'NONE',  ( 0.000000000000000000, 0.000000000000000000, 1.000000000000000000 ) ) ;
#7510=ORIENTED_EDGE ( 'NONE', *, *, #5362, .F. ) ;
#7511=EDGE_CURVE ( 'NONE', #4197, #3508, #7505, .T. ) ;
#7513=EDGE_CURVE ( 'NONE', #10985, #11120, #7157, .T. ) ;
#7522=VECTOR ( 'NONE', #2061, 1000.000000000000000 ) ;
#7528=DIRECTION ( 'NONE',  ( 1.000000000000000000, 0.000000000000000000, 0.000000000000000000 ) ) ;
#7533=CARTESIAN_POINT ( 'NONE',  ( 2.740003299868484010, -9.490919315500217834, 11.55877992729661585 ) ) ;
#7534=DIRECTION ( 'NONE',  ( -1.000000000000000000, 0.000000000000000000, -0.000000000000000000 ) ) ;
#7542=DIRECTION ( 'NONE',  ( 1.000000000000000000, 0.000000000000000000, -0.000000000000000000 ) ) ;
#7547=APPLICATION_CONTEXT ( 'automotive_design' ) ;
#7554=ORIENTED_EDGE ( 'NONE', *, *, #130, .F. ) ;
#7571=CARTESIAN_POINT ( 'NONE',  ( 2.789999999999999147, 14.59528211760002137, -3.120158876139080828 ) ) ;
#7572=VERTEX_POINT ( 'NONE', #4431 ) ;
#7586=ADVANCED_FACE ( 'NONE', ( #5661 ), #1689, .T. ) ;
#7590=AXIS2_PLACEMENT_3D ( 'NONE', #1148, #5918, #8070 ) ;
#7596=CARTESIAN_POINT ( 'NONE',  ( 2.764680872513935128, -5.229914364928447412, 13.68080036884346917 ) ) ;
#7604=CIRCLE ( 'NONE', #2202, 2.524999999999999467 ) ;
#7609=CARTESIAN_POINT ( 'NONE',  ( 2.246812931352481169, -11.42270873787301610, 12.54666350726119717 ) ) ;
#7610=DIRECTION ( 'NONE',  ( 0.000000000000000000, 0.000000000000000000, 1.000000000000000000 ) ) ;
#7613=LINE ( 'NONE', #8605, #157 ) ;
#7619=CARTESIAN_POINT ( 'NONE',  ( 2.764680872513208154, 9.232963481057765875, 11.36963888406690870 ) ) ;
#7625=ORIENTED_EDGE ( 'NONE', *, *, #10486, .T. ) ;
#7627=CARTESIAN_POINT ( 'NONE',  ( 2.782650468023970536, -14.24968354755769973, 2.217353748341881481 ) ) ;
#7631=DIRECTION ( 'NONE',  ( -1.000000000000000000, -0.000000000000000000, -0.000000000000000000 ) ) ;
#7634=DIRECTION ( 'NONE',  ( 1.000000000000000000, -0.000000000000000000, -0.000000000000000000 ) ) ;
#7635=LINE ( 'NONE', #628, #10997 ) ;
#7636=CYLINDRICAL_SURFACE ( 'NONE', #8436, 8.400000000000000355 ) ;
#7638=EDGE_CURVE ( 'NONE', #8287, #6623, #12404, .T. ) ;
#7642=CARTESIAN_POINT ( 'NONE',  ( 1.749999999999999778, -17.39253030560838198, -4.458161950358684678 ) ) ;
#7643=CARTESIAN_POINT ( 'NONE',  ( 2.697960371751379594, -11.73065272960056049, -9.756102650610364080 ) ) ;
#7650=CARTESIAN_POINT ( 'NONE',  ( 2.764680872515352217, 14.46287784598617243, 2.311161484776605324 ) ) ;
#7657=EDGE_LOOP ( 'NONE', ( #12164, #13793, #1438, #6995, #11289, #9610 ) ) ;
#7665=CARTESIAN_POINT ( 'NONE',  ( 0.9041604711286022056, -12.27244837507622499, 12.77651625388895162 ) ) ;
#7672=FACE_OUTER_BOUND ( 'NONE', #9026, .T. ) ;
#7673=ORIENTED_EDGE ( 'NONE', *, *, #14370, .T. ) ;
#7675=B_SPLINE_CURVE_WITH_KNOTS ( 'NONE', 3,
 ( #8371, #3687, #13050, #14301, #2617, #10835, #5012, #8529 ),
 .UNSPECIFIED., .F., .F.,
 ( 4, 2, 2, 4 ),
 ( 2.154797737796103340E-07, 0.001895231411415141797, 0.002842739377235821516, 0.003790247343056500802 ),
 .UNSPECIFIED. ) ;
#7703=DIRECTION ( 'NONE',  ( -1.000000000000000000, 0.000000000000000000, 0.000000000000000000 ) ) ;
#7707=EDGE_CURVE ( 'NONE', #11802, #2246, #6237, .T. ) ;
#7713=CARTESIAN_POINT ( 'NONE',  ( 0.9041604898882311669, 17.01651022436369942, -4.928563447326111735 ) ) ;
#7714=CARTESIAN_POINT ( 'NONE',  ( 2.740003299868483566, -11.55877992729658565, -9.490919315500255138 ) ) ;
#7715=CIRCLE ( 'NONE', #12610, 17.95481323787947403 ) ;
#7716=VERTEX_POINT ( 'NONE', #11843 ) ;
#7723=LINE ( 'NONE', #12408, #12932 ) ;
#7725=VERTEX_POINT ( 'NONE', #1108 ) ;
#7728=ORIENTED_EDGE ( 'NONE', *, *, #5653, .F. ) ;
#7731=VERTEX_POINT ( 'NONE', #13000 ) ;
#7732=AXIS2_PLACEMENT_3D ( 'NONE', #6281, #2821, #2975 ) ;
#7741=DIRECTION ( 'NONE',  ( 0.000000000000000000, 0.000000000000000000, -1.000000000000000000 ) ) ;
#7748=AXIS2_PLACEMENT_3D ( 'NONE', #7947, #4271, #6720 ) ;
#7766=AXIS2_PLACEMENT_3D ( 'NONE', #3601, #9438, #3456 ) ;
#7777=DIRECTION ( 'NONE',  ( -1.000000000000000000, -0.000000000000000000, -0.000000000000000000 ) ) ;
#7782=DIRECTION ( 'NONE',  ( 0.000000000000000000, 0.000000000000000000, 1.000000000000000000 ) ) ;
#7784=CARTESIAN_POINT ( 'NONE',  ( 1.039999999999996261, 4.458161950358501713, 17.39253030560843172 ) ) ;
#7787=CARTESIAN_POINT ( 'NONE',  ( 2.789999999999999147, 1.948757464274172513, 13.87420763704361804 ) ) ;
#7795=VECTOR ( 'NONE', #2451, 1000.000000000000000 ) ;
#7801=CARTESIAN_POINT ( 'NONE',  ( 2.789999999999999147, -13.40591150984221080, -7.739906618939849103 ) ) ;
#7807=CARTESIAN_POINT ( 'NONE',  ( 2.764680872515352661, -9.232963481057844035, 11.36963888406684298 ) ) ;
#7808=ORIENTED_EDGE ( 'NONE', *, *, #3186, .F. ) ;
#7812=AXIS2_PLACEMENT_3D ( 'NONE', #14402, #14246, #3870 ) ;
#7817=B_SPLINE_CURVE_WITH_KNOTS ( 'NONE', 3,
 ( #11077, #11145, #620, #12143 ),
 .UNSPECIFIED., .F., .F.,
 ( 4, 4 ),
 ( 2.451234579287542699E-07, 0.0006917187676826498915 ),
 .UNSPECIFIED. ) ;
#7825=DIRECTION ( 'NONE',  ( -1.000000000000000000, -0.000000000000000000, -0.000000000000000000 ) ) ;
#7827=EDGE_LOOP ( 'NONE', ( #4192, #13937, #14547, #2184, #8460, #5410 ) ) ;
#7828=CARTESIAN_POINT ( 'NONE',  ( 2.508169649284525793, 3.072260951847751720, -15.84037596932104464 ) ) ;
#7830=LINE ( 'NONE', #14901, #3599 ) ;
#7831=ORIENTED_EDGE ( 'NONE', *, *, #2531, .T. ) ;
#7832=CIRCLE ( 'NONE', #4647, 14.01039946648073986 ) ;
#7836=CARTESIAN_POINT ( 'NONE',  ( 2.789999999999999147, -11.36963888406680923, -9.232963481057881339 ) ) ;
#7841=CARTESIAN_POINT ( 'NONE',  ( 2.764680872513937349, -13.68080036884344963, -5.229914364928496262 ) ) ;
#7844=CARTESIAN_POINT ( 'NONE',  ( 2.789999999999999147, -9.232963481057844035, 11.36963888406684298 ) ) ;
#7846=DIRECTION ( 'NONE',  ( 1.000000000000000000, 0.000000000000000000, 0.000000000000000000 ) ) ;
#7848=VECTOR ( 'NONE', #8304, 1000.000000000000000 ) ;
#7849=EDGE_CURVE ( 'NONE', #7151, #12400, #81, .T. ) ;
#7857=EDGE_LOOP ( 'NONE', ( #9985, #2165, #7886, #10347 ) ) ;
#7858=VERTEX_POINT ( 'NONE', #2867 ) ;
#7860=TOROIDAL_SURFACE ( 'NONE', #11528, 14.01039946648073986, 8.000000000000000000 ) ;
#7861=CARTESIAN_POINT ( 'NONE',  ( 1.885839528871396054, -12.77651625388907775, 12.27244837507608466 ) ) ;
#7863=CARTESIAN_POINT ( 'NONE',  ( 2.789999999999999147, -3.120158876139132342, 14.59528211760001071 ) ) ;
#7868=AXIS2_PLACEMENT_3D ( 'NONE', #1204, #13965, #3431 ) ;
#7873=FACE_OUTER_BOUND ( 'NONE', #5982, .T. ) ;
#7879=EDGE_CURVE ( 'NONE', #6222, #6770, #11626, .T. ) ;
#7881=ORIENTED_EDGE ( 'NONE', *, *, #14598, .T. ) ;
#7886=ORIENTED_EDGE ( 'NONE', *, *, #4383, .T. ) ;
#7887=DIRECTION ( 'NONE',  ( 1.000000000000000000, 0.000000000000000000, 0.000000000000000000 ) ) ;
#7899=EDGE_CURVE ( 'NONE', #1420, #9357, #4038, .T. ) ;
#7902=DIRECTION ( 'NONE',  ( -1.000000000000000000, 0.000000000000000000, -0.000000000000000000 ) ) ;
#7907=LINE ( 'NONE', #12583, #8005 ) ;
#7909=ORIENTED_EDGE ( 'NONE', *, *, #7707, .T. ) ;
#7915=LINE ( 'NONE', #7844, #6247 ) ;
#7935=DIRECTION ( 'NONE',  ( -1.000000000000000000, 0.000000000000000000, 0.000000000000000000 ) ) ;
#7936=CARTESIAN_POINT ( 'NONE',  ( 0.000000000000000000, 7.739906618939895289, -13.40591150984218416 ) ) ;
#7938=CYLINDRICAL_SURFACE ( 'NONE', #6517, 8.400000000000000355 ) ;
#7942=DIRECTION ( 'NONE',  ( -1.000000000000000000, -0.000000000000000000, -0.000000000000000000 ) ) ;
#7947=CARTESIAN_POINT ( 'NONE',  ( 0.000000000000000000, -15.47981323787947794, -1.080949580976661932E-13 ) ) ;
#7952=EDGE_LOOP ( 'NONE', ( #8424, #8868, #10077, #5608, #13078, #14800 ) ) ;
#7953=ORIENTED_EDGE ( 'NONE', *, *, #13788, .T. ) ;
#7958=CIRCLE ( 'NONE', #5281, 2.524999999999999467 ) ;
#7959=CARTESIAN_POINT ( 'NONE',  ( 0.000000000000000000, 0.000000000000000000, 0.000000000000000000 ) ) ;
#7961=CARTESIAN_POINT ( 'NONE',  ( 50.00050000000000239, 0.000000000000000000, 0.000000000000000000 ) ) ;
#7963=CARTESIAN_POINT ( 'NONE',  ( 1.749999999999999778, -4.835383649608602674, 17.29145405592687013 ) ) ;
#7967=CARTESIAN_POINT ( 'NONE',  ( 2.246812880117044386, 3.619024283482299875, -16.57708379306440349 ) ) ;
#7981=DIRECTION ( 'NONE',  ( 0.000000000000000000, 0.000000000000000000, 1.000000000000000000 ) ) ;
#7985=CARTESIAN_POINT ( 'NONE',  ( 0.000000000000000000, -5.404747904883309660E-14, 15.47981323787947794 ) ) ;
#7991=DIRECTION ( 'NONE',  ( -1.000000000000000000, 0.000000000000000000, -0.000000000000000000 ) ) ;
#7996=VERTEX_POINT ( 'NONE', #12545 ) ;
#7997=AXIS2_PLACEMENT_3D ( 'NONE', #10251, #3327, #13781 ) ;
#7999=VERTEX_POINT ( 'NONE', #12312 ) ;
#8001=CARTESIAN_POINT ( 'NONE',  ( 1.749999999999999778, 0.000000000000000000, 0.000000000000000000 ) ) ;
#8005=VECTOR ( 'NONE', #12354, 1000.000000000000000 ) ;
#8007=CARTESIAN_POINT ( 'NONE',  ( 1.749999999999999778, -12.83329210556822453, -12.55714665600001290 ) ) ;
#8014=CIRCLE ( 'NONE', #9249, 17.95481323787947758 ) ;
#8017=ORIENTED_EDGE ( 'NONE', *, *, #14660, .F. ) ;
#8033=ADVANCED_FACE ( 'NONE', ( #2948 ), #7636, .T. ) ;
#8035=CIRCLE ( 'NONE', #3377, 14.01039946648074341 ) ;
#8044=AXIS2_PLACEMENT_3D ( 'NONE', #8117, #10641, #1265 ) ;
#8045=CARTESIAN_POINT ( 'NONE',  ( 0.000000000000000000, 0.000000000000000000, 0.000000000000000000 ) ) ;
#8048=CARTESIAN_POINT ( 'NONE',  ( 2.337784062669522989, 3.429166897524429825, 16.32199768300080933 ) ) ;
#8053=CYLINDRICAL_SURFACE ( 'NONE', #14544, 17.95481323787947403 ) ;
#8056=ORIENTED_EDGE ( 'NONE', *, *, #6386, .F. ) ;
#8061=ORIENTED_EDGE ( 'NONE', *, *, #6548, .F. ) ;
#8064=ORIENTED_EDGE ( 'NONE', *, *, #5019, .F. ) ;
#8065=CARTESIAN_POINT ( 'NONE',  ( 0.007327532539344703763, -14.24942254254691143, 2.217238903388513371 ) ) ;
#8066=DIRECTION ( 'NONE',  ( 0.000000000000000000, 0.000000000000000000, -1.000000000000000000 ) ) ;
#8068=EDGE_CURVE ( 'NONE', #406, #799, #631, .T. ) ;
#8069=CARTESIAN_POINT ( 'NONE',  ( 0.007349531976027265379, 2.217353748342130615, -14.24968354755766420 ) ) ;
#8070=DIRECTION ( 'NONE',  ( 0.000000000000000000, 0.000000000000000000, 1.000000000000000000 ) ) ;
#8085=B_SPLINE_CURVE_WITH_KNOTS ( 'NONE', 3,
 ( #374, #5093, #8224, #14228, #13051, #2540, #13223, #1303 ),
 .UNSPECIFIED., .F., .F.,
 ( 4, 2, 2, 4 ),
 ( 2.445728210242702351E-07, 0.001895260649874686140, 0.002842768688401515337, 0.003790276726928345184 ),
 .UNSPECIFIED. ) ;
#8086=CARTESIAN_POINT ( 'NONE',  ( 1.039999999999997815, -12.55714665599996316, 12.83329210556827604 ) ) ;
#8088=TOROIDAL_SURFACE ( 'NONE', #1455, 14.01039946648074341, 8.000000000000000000 ) ;
#8089=B_SPLINE_CURVE_WITH_KNOTS ( 'NONE', 3,
 ( #8890, #12349, #7967, #7828, #12513, #2131, #5454, #754 ),
 .UNSPECIFIED., .F., .F.,
 ( 4, 2, 2, 4 ),
 ( 4.663089412828908672E-07, 0.001898630173449110652, 0.002847712105703028435, 0.003796794037956946651 ),
 .UNSPECIFIED. ) ;
#8094=CARTESIAN_POINT ( 'NONE',  ( 0.2076373213218624669, 15.57879356040245078, -2.899259574942687046 ) ) ;
#8099=ORIENTED_EDGE ( 'NONE', *, *, #6386, .T. ) ;
#8103=ORIENTED_EDGE ( 'NONE', *, *, #8336, .F. ) ;
#8105=CARTESIAN_POINT ( 'NONE',  ( 2.789999999999999147, 7.739906618939707883, 13.40591150984229252 ) ) ;
#8117=CARTESIAN_POINT ( 'NONE',  ( 2.789999999999999147, -14.19996452731185776, -4.595504208220178022 ) ) ;
#8121=LINE ( 'NONE', #10579, #1235 ) ;
#8124=CARTESIAN_POINT ( 'NONE',  ( 1.749999999999999778, 0.000000000000000000, 0.000000000000000000 ) ) ;
#8129=CARTESIAN_POINT ( 'NONE',  ( 2.236220367026671152, -16.15122426806985345, -5.139875429512027694 ) ) ;
#8137=CARTESIAN_POINT ( 'NONE',  ( 1.039999999999997593, 0.000000000000000000, 0.000000000000000000 ) ) ;
#8147=DIRECTION ( 'NONE',  ( -1.000000000000000000, 0.000000000000000000, 0.000000000000000000 ) ) ;
#8150=EDGE_CURVE ( 'NONE', #9201, #10080, #14946, .T. ) ;
#8152=CARTESIAN_POINT ( 'NONE',  ( 0.2818302809372403850, -10.58084377126614584, -12.18203740414278258 ) ) ;
#8154=DIRECTION ( 'NONE',  ( 0.000000000000000000, 0.000000000000000000, 1.000000000000000000 ) ) ;
#8158=VECTOR ( 'NONE', #13792, 1000.000000000000000 ) ;
#8162=CARTESIAN_POINT ( 'NONE',  ( 1.749999999999999778, 4.835383649608716361, -17.29145405592683815 ) ) ;
#8168=DIRECTION ( 'NONE',  ( -1.000000000000000000, -0.000000000000000000, -0.000000000000000000 ) ) ;
#8178=ORIENTED_EDGE ( 'NONE', *, *, #2129, .T. ) ;
#8181=CARTESIAN_POINT ( 'NONE',  ( 0.2818303916520942254, -5.259531939870306871, 15.25429862889480148 ) ) ;
#8183=CARTESIAN_POINT ( 'NONE',  ( 1.749999999999999778, 4.835383649608472112, 17.29145405592690210 ) ) ;
#8185=CARTESIAN_POINT ( 'NONE',  ( 0.000000000000000000, 11.04103753892271733, 8.624777288397844188 ) ) ;
#8187=EDGE_CURVE ( 'NONE', #6211, #9602, #4292, .T. ) ;
#8188=VERTEX_POINT ( 'NONE', #6455 ) ;
#8191=CARTESIAN_POINT ( 'NONE',  ( 0.000000000000000000, 5.249430348645754307, 12.98979500319696534 ) ) ;
#8194=ORIENTED_EDGE ( 'NONE', *, *, #5998, .T. ) ;
#8202=CARTESIAN_POINT ( 'NONE',  ( 2.764680872515352661, 9.232963481057920418, -11.36963888406677725 ) ) ;
#8204=DIRECTION ( 'NONE',  ( -1.000000000000000000, -0.000000000000000000, -0.000000000000000000 ) ) ;
#8209=CIRCLE ( 'NONE', #12133, 2.524999999999997691 ) ;
#8212=ORIENTED_EDGE ( 'NONE', *, *, #8495, .F. ) ;
#8215=ORIENTED_EDGE ( 'NONE', *, *, #2032, .T. ) ;
#8216=ORIENTED_EDGE ( 'NONE', *, *, #11905, .F. ) ;
#8217=ORIENTED_EDGE ( 'NONE', *, *, #14598, .F. ) ;
#8224=CARTESIAN_POINT ( 'NONE',  ( 2.597943782557558645, -10.28947301956273996, -12.05486625177582560 ) ) ;
#8227=CARTESIAN_POINT ( 'NONE',  ( 2.789999999999999147, 13.68080036884348516, 5.229914364928400339 ) ) ;
#8229=CIRCLE ( 'NONE', #7997, 2.524999999999999467 ) ;
#8230=EDGE_CURVE ( 'NONE', #228, #212, #5176, .T. ) ;
#8232=ORIENTED_EDGE ( 'NONE', *, *, #1768, .F. ) ;
#8235=VERTEX_POINT ( 'NONE', #14607 ) ;
#8236=ORIENTED_EDGE ( 'NONE', *, *, #5994, .T. ) ;
#8241=CARTESIAN_POINT ( 'NONE',  ( 0.000000000000000000, 13.87420763704361626, 1.948757464274225137 ) ) ;
#8251=( GEOMETRIC_REPRESENTATION_CONTEXT ( 3 ) GLOBAL_UNCERTAINTY_ASSIGNED_CONTEXT ( ( #391 ) ) GLOBAL_UNIT_ASSIGNED_CONTEXT ( ( #9778, #3939, #6392 ) ) REPRESENTATION_CONTEXT ( 'NONE', 'WORKASPACE' ) );
#8255=CARTESIAN_POINT ( 'NONE',  ( 0.1920562174424399748, -12.05486625177564797, -10.28947301956294780 ) ) ;
#8261=DIRECTION ( 'NONE',  ( -1.000000000000000000, -0.000000000000000000, -0.000000000000000000 ) ) ;
#8262=CIRCLE ( 'NONE', #10239, 14.01039946648074341 ) ;
#8271=ORIENTED_EDGE ( 'NONE', *, *, #13622, .F. ) ;
#8273=DIRECTION ( 'NONE',  ( 0.000000000000000000, 0.000000000000000000, -1.000000000000000000 ) ) ;
#8276=CARTESIAN_POINT ( 'NONE',  ( 1.039999999999999369, 12.55714665599987079, 12.83329210556836308 ) ) ;
#8285=CARTESIAN_POINT ( 'NONE',  ( 2.764680872513205934, -11.36963888406694068, 9.232963481057725019 ) ) ;
#8287=VERTEX_POINT ( 'NONE', #13825 ) ;
#8291=CYLINDRICAL_SURFACE ( 'NONE', #592, 8.400000000000000355 ) ;
#8294=CIRCLE ( 'NONE', #9280, 14.01039946648073986 ) ;
#8302=CARTESIAN_POINT ( 'NONE',  ( 2.582362678678087331, -2.899259574942854023, 15.57879356040262309 ) ) ;
#8304=DIRECTION ( 'NONE',  ( -1.000000000000000000, -0.000000000000000000, 0.000000000000000000 ) ) ;
#8305=AXIS2_PLACEMENT_3D ( 'NONE', #2798, #407, #7498 ) ;
#8308=EDGE_LOOP ( 'NONE', ( #9916, #7142, #10014, #743 ) ) ;
#8312=AXIS2_PLACEMENT_3D ( 'NONE', #4575, #9396, #6948 ) ;
#8317=ORIENTED_EDGE ( 'NONE', *, *, #12278, .T. ) ;
#8319=EDGE_CURVE ( 'NONE', #5935, #799, #10297, .T. ) ;
#8326=CARTESIAN_POINT ( 'NONE',  ( 2.646101151984011857, -14.59528211758545524, 5.279841123860813390 ) ) ;
#8336=EDGE_CURVE ( 'NONE', #11120, #10268, #6988, .T. ) ;
#8345=CYLINDRICAL_SURFACE ( 'NONE', #2374, 17.95481323787947403 ) ;
#8351=DIRECTION ( 'NONE',  ( 0.000000000000000000, 0.000000000000000000, 1.000000000000000000 ) ) ;
#8352=CARTESIAN_POINT ( 'NONE',  ( 0.000000000000000000, 0.000000000000000000, 0.000000000000000000 ) ) ;
#8369=DIRECTION ( 'NONE',  ( 0.000000000000000000, 0.000000000000000000, 1.000000000000000000 ) ) ;
#8371=CARTESIAN_POINT ( 'NONE',  ( 0.02531912748631424959, 14.46287784598617243, 2.311161484776605324 ) ) ;
#8387=DIRECTION ( 'NONE',  ( 1.000000000000000000, -0.000000000000000000, -0.000000000000000000 ) ) ;
#8395=ORIENTED_EDGE ( 'NONE', *, *, #4802, .T. ) ;
#8405=DIRECTION ( 'NONE',  ( 0.000000000000000000, 0.000000000000000000, 1.000000000000000000 ) ) ;
#8408=DIRECTION ( 'NONE',  ( -1.000000000000000000, -0.000000000000000000, -0.000000000000000000 ) ) ;
#8414=EDGE_CURVE ( 'NONE', #13214, #4401, #2104, .T. ) ;
#8416=ORIENTED_EDGE ( 'NONE', *, *, #8836, .T. ) ;
#8424=ORIENTED_EDGE ( 'NONE', *, *, #10840, .F. ) ;
#8427=EDGE_CURVE ( 'NONE', #10827, #159, #7424, .T. ) ;
#8428=EDGE_CURVE ( 'NONE', #1826, #7716, #12083, .T. ) ;
#8432=CARTESIAN_POINT ( 'NONE',  ( 0.9041604711286044260, 12.27244837507631381, -12.77651625388886281 ) ) ;
#8436=AXIS2_PLACEMENT_3D ( 'NONE', #6475, #1720, #11159 ) ;
#8438=TOROIDAL_SURFACE ( 'NONE', #10407, 14.01039946648074341, 8.000000000000000000 ) ;
#8444=EDGE_CURVE ( 'NONE', #6351, #3683, #8209, .T. ) ;
#8446=CARTESIAN_POINT ( 'NONE',  ( 2.789999999999999147, 0.000000000000000000, 0.000000000000000000 ) ) ;
#8450=CARTESIAN_POINT ( 'NONE',  ( 2.697960371751379149, 11.73065272960063155, 9.756102650610282367 ) ) ;
#8452=VERTEX_POINT ( 'NONE', #10520 ) ;
#8458=CARTESIAN_POINT ( 'NONE',  ( 0.7686372590627860157, -16.74220655292933913, -5.021526291670494579 ) ) ;
#8460=ORIENTED_EDGE ( 'NONE', *, *, #12351, .T. ) ;
#8466=FACE_OUTER_BOUND ( 'NONE', #5731, .T. ) ;
#8476=AXIS2_PLACEMENT_3D ( 'NONE', #14780, #11236, #624 ) ;
#8479=CARTESIAN_POINT ( 'NONE',  ( 2.789999999999999147, 8.624777288397799779, 11.04103753892274753 ) ) ;
#8482=CARTESIAN_POINT ( 'NONE',  ( 2.789999999999999147, 13.40591150984237245, -7.739906618939567551 ) ) ;
#8494=ORIENTED_EDGE ( 'NONE', *, *, #4796, .F. ) ;
#8495=EDGE_CURVE ( 'NONE', #14323, #6652, #6257, .T. ) ;
#8500=CIRCLE ( 'NONE', #1888, 17.95481323787947758 ) ;
#8502=AXIS2_PLACEMENT_3D ( 'NONE', #2013, #7777, #6699 ) ;
#8503=CARTESIAN_POINT ( 'NONE',  ( 1.039999999999997593, 0.000000000000000000, 0.000000000000000000 ) ) ;
#8507=CARTESIAN_POINT ( 'NONE',  ( 2.789999999999999147, -7.739906618939614624, -13.40591150984234581 ) ) ;
#8510=CARTESIAN_POINT ( 'NONE',  ( 2.646101151981377075, 14.59528211759998406, 5.279841123860917307 ) ) ;
#8514=AXIS2_PLACEMENT_3D ( 'NONE', #1508, #8646, #13332 ) ;
#8518=EDGE_CURVE ( 'NONE', #13761, #10809, #7492, .T. ) ;
#8524=ORIENTED_EDGE ( 'NONE', *, *, #14171, .T. ) ;
#8527=ADVANCED_FACE ( 'NONE', ( #13397 ), #14565, .T. ) ;
#8529=CARTESIAN_POINT ( 'NONE',  ( 1.039999999999996483, 17.39253030560841395, 4.458161950358563885 ) ) ;
#8530=CARTESIAN_POINT ( 'NONE',  ( 2.021362756903525959, -4.022333916463714409, 17.00993931356759603 ) ) ;
#8536=VERTEX_POINT ( 'NONE', #12250 ) ;
#8537=AXIS2_PLACEMENT_3D ( 'NONE', #12660, #9214, #6905 ) ;
#8540=B_SPLINE_CURVE_WITH_KNOTS ( 'NONE', 3,
 ( #8618, #2940, #7627, #12378 ),
 .UNSPECIFIED., .F., .F.,
 ( 4, 4 ),
 ( 0.005123713096549405849, 0.005814346476695844007 ),
 .UNSPECIFIED. ) ;
#8544=DIRECTION ( 'NONE',  ( -1.000000000000000000, -0.000000000000000000, -0.000000000000000000 ) ) ;
#8554=VERTEX_POINT ( 'NONE', #11093 ) ;
#8561=CARTESIAN_POINT ( 'NONE',  ( 0.4522159468065707899, 12.42068120944081322, 11.13074453164208144 ) ) ;
#8562=CARTESIAN_POINT ( 'NONE',  ( 2.715264182578264407, -14.31752701692933272, -5.299647274067250891 ) ) ;
#8565=CARTESIAN_POINT ( 'NONE',  ( 2.782650442329439588, 9.045126717605779021, 11.23191127083866725 ) ) ;
#8569=VECTOR ( 'NONE', #14816, 1000.000000000000000 ) ;
#8580=EDGE_CURVE ( 'NONE', #1432, #3477, #992, .T. ) ;
#8581=ORIENTED_EDGE ( 'NONE', *, *, #7899, .T. ) ;
#8584=EDGE_CURVE ( 'NONE', #5623, #159, #1878, .T. ) ;
#8588=CYLINDRICAL_SURFACE ( 'NONE', #3997, 2.524999999999999467 ) ;
#8589=VERTEX_POINT ( 'NONE', #10171 ) ;
#8591=CARTESIAN_POINT ( 'NONE',  ( 2.782672435525939125, 11.23174270417329268, 9.044896821682240073 ) ) ;
#8595=CYLINDRICAL_SURFACE ( 'NONE', #4334, 17.95481323787947403 ) ;
#8600=CYLINDRICAL_SURFACE ( 'NONE', #6284, 2.524999999999999467 ) ;
#8605=CARTESIAN_POINT ( 'NONE',  ( 1.394999999999999574, -17.29145405592692342, 4.835383649608410828 ) ) ;
#8614=EDGE_CURVE ( 'NONE', #3527, #4006, #9054, .T. ) ;
#8618=CARTESIAN_POINT ( 'NONE',  ( 2.789999999999999147, -13.87420763704362514, 1.948757464274123885 ) ) ;
#8632=CARTESIAN_POINT ( 'NONE',  ( 1.039999999999996483, 17.29145405592695539, -4.835383649608292700 ) ) ;
#8638=EDGE_CURVE ( 'NONE', #8452, #13251, #9788, .T. ) ;
#8639=CIRCLE ( 'NONE', #2021, 17.95481323787947758 ) ;
#8641=DIRECTION ( 'NONE',  ( 0.000000000000000000, 0.000000000000000000, 1.000000000000000000 ) ) ;
#8645=FACE_OUTER_BOUND ( 'NONE', #5293, .T. ) ;
#8646=DIRECTION ( 'NONE',  ( -1.000000000000000000, 0.000000000000000000, -0.000000000000000000 ) ) ;
#8650=ORIENTED_EDGE ( 'NONE', *, *, #660, .T. ) ;
#8651=DIRECTION ( 'NONE',  ( 0.000000000000000000, 0.000000000000000000, 1.000000000000000000 ) ) ;
#8663=CARTESIAN_POINT ( 'NONE',  ( 0.000000000000000000, -8.624777288397881492, 11.04103753892268891 ) ) ;
#8664=CARTESIAN_POINT ( 'NONE',  ( 0.04999671152047703571, -14.75565684666127986, 2.439987328296917557 ) ) ;
#8666=EDGE_LOOP ( 'NONE', ( #3586, #341, #6741, #6010, #13227, #8939, #7728, #496, #3126, #11228, #6818, #7420, #13682, #11620, #2074, #419, #11508, #5425, #11672, #4339, #5215, #13942, #3920, #10995, #13589, #2251, #1216 ) ) ;
#8669=CARTESIAN_POINT ( 'NONE',  ( 0.02531912748631468327, -14.46287784598615644, -2.311161484776706576 ) ) ;
#8670=CARTESIAN_POINT ( 'NONE',  ( 0.007327532539345395050, -2.217238903388463189, -14.24942254254691854 ) ) ;
#8675=EDGE_CURVE ( 'NONE', #7151, #10675, #4065, .T. ) ;
#8682=VECTOR ( 'NONE', #10215, 1000.000000000000000 ) ;
#8692=B_SPLINE_CURVE_WITH_KNOTS ( 'NONE', 3,
 ( #12230, #10005, #6546, #12145 ),
 .UNSPECIFIED., .F., .F.,
 ( 4, 4 ),
 ( 2.159563976726664397E-07, 0.0006916893629248962961 ),
 .UNSPECIFIED. ) ;
#8699=CARTESIAN_POINT ( 'NONE',  ( 0.02531912748464674665, 11.36963888406700285, -9.232963481057645083 ) ) ;
#8702=CARTESIAN_POINT ( 'NONE',  ( 2.789999999999999147, 11.36963888406687317, 9.232963481057801403 ) ) ;
#8707=AXIS2_PLACEMENT_3D ( 'NONE', #4878, #8168, #2327 ) ;
#8712=DIRECTION ( 'NONE',  ( 0.000000000000000000, 0.000000000000000000, 1.000000000000000000 ) ) ;
#8724=VERTEX_POINT ( 'NONE', #2097 ) ;
#8725=ORIENTED_EDGE ( 'NONE', *, *, #8584, .T. ) ;
#8726=VERTEX_POINT ( 'NONE', #5876 ) ;
#8730=CARTESIAN_POINT ( 'NONE',  ( 0.007349557670559583172, 11.23191127083863350, 9.045126717605816324 ) ) ;
#8743=CARTESIAN_POINT ( 'NONE',  ( 1.749999999999999778, 0.000000000000000000, 0.000000000000000000 ) ) ;
#8744=CARTESIAN_POINT ( 'NONE',  ( 2.789999999999999147, 9.999777909380087593, -11.07980565117269833 ) ) ;
#8751=DIRECTION ( 'NONE',  ( -1.000000000000000000, -0.000000000000000000, -0.000000000000000000 ) ) ;
#8759=DIRECTION ( 'NONE',  ( 0.000000000000000000, 0.000000000000000000, 1.000000000000000000 ) ) ;
#8781=DIRECTION ( 'NONE',  ( 1.000000000000000000, 0.000000000000000000, 0.000000000000000000 ) ) ;
#8786=AXIS2_PLACEMENT_3D ( 'NONE', #9344, #5816, #4590 ) ;
#8802=LINE ( 'NONE', #5370, #8158 ) ;
#8808=VERTEX_POINT ( 'NONE', #12991 ) ;
#8812=CIRCLE ( 'NONE', #12495, 4.000000000000000000 ) ;
#8821=EDGE_CURVE ( 'NONE', #11883, #6223, #14314, .T. ) ;
#8826=CARTESIAN_POINT ( 'NONE',  ( 1.039999999999996039, -12.83329210556840394, 12.55714665599982816 ) ) ;
#8832=CARTESIAN_POINT ( 'NONE',  ( 2.764680872515352661, 9.232963481057920418, -11.36963888406677725 ) ) ;
#8836=EDGE_CURVE ( 'NONE', #3473, #1249, #12727, .T. ) ;
#8844=ORIENTED_EDGE ( 'NONE', *, *, #6921, .T. ) ;
#8850=LINE ( 'NONE', #13543, #1866 ) ;
#8862=CARTESIAN_POINT ( 'NONE',  ( 2.789999999999999147, 14.59528211759997696, 3.120158876139284665 ) ) ;
#8866=ORIENTED_EDGE ( 'NONE', *, *, #6558, .F. ) ;
#8868=ORIENTED_EDGE ( 'NONE', *, *, #2424, .F. ) ;
#8876=ORIENTED_EDGE ( 'NONE', *, *, #12295, .F. ) ;
#8880=CARTESIAN_POINT ( 'NONE',  ( 1.394999999999998685, 17.29145405592695894, -4.835383649608291812 ) ) ;
#8884=LINE ( 'NONE', #14892, #8569 ) ;
#8890=CARTESIAN_POINT ( 'NONE',  ( 1.749999999999999778, 4.458161950358745074, -17.39253030560836777 ) ) ;
#8893=EDGE_CURVE ( 'NONE', #13265, #4412, #8692, .T. ) ;
#8896=VERTEX_POINT ( 'NONE', #9782 ) ;
#8899=ORIENTED_EDGE ( 'NONE', *, *, #13238, .F. ) ;
#8902=DIRECTION ( 'NONE',  ( 0.000000000000000000, -1.717547996016640980E-15, -1.000000000000000000 ) ) ;
#8906=LINE ( 'NONE', #14535, #9420 ) ;
#8910=LINE ( 'NONE', #12452, #11589 ) ;
#8916=CARTESIAN_POINT ( 'NONE',  ( 1.039999999999997593, 4.835383649608715473, -17.29145405592683815 ) ) ;
#8920=ORIENTED_EDGE ( 'NONE', *, *, #13134, .F. ) ;
#8922=ORIENTED_EDGE ( 'NONE', *, *, #3452, .T. ) ;
#8925=CARTESIAN_POINT ( 'NONE',  ( 0.02531912748606228100, 5.229914364928351489, 13.68080036884350292 ) ) ;
#8932=CARTESIAN_POINT ( 'NONE',  ( 1.039999999999997593, 0.000000000000000000, 0.000000000000000000 ) ) ;
#8937=CARTESIAN_POINT ( 'NONE',  ( 0.02531912748286561932, 13.68080036884348516, 5.229914364928400339 ) ) ;
#8939=ORIENTED_EDGE ( 'NONE', *, *, #4388, .F. ) ;
#8944=ORIENTED_EDGE ( 'NONE', *, *, #8068, .T. ) ;
#8949=VERTEX_POINT ( 'NONE', #4010 ) ;
#8952=CARTESIAN_POINT ( 'NONE',  ( 2.789999999999999147, 13.40591150984226587, 7.739906618939754956 ) ) ;
#8958=DIRECTION ( 'NONE',  ( -1.000000000000000000, -0.000000000000000000, -0.000000000000000000 ) ) ;
#8959=EDGE_CURVE ( 'NONE', #1894, #12582, #3014, .T. ) ;
#8965=CARTESIAN_POINT ( 'NONE',  ( 2.781248467066446572, 13.40591150985955871, -5.214906618939568972 ) ) ;
#8971=B_SPLINE_CURVE_WITH_KNOTS ( 'NONE', 3,
 ( #4281, #5448, #11494, #13961 ),
 .UNSPECIFIED., .F., .F.,
 ( 4, 4 ),
 ( 1.984117560508715598E-07, 0.0009182716802120147702 ),
 .UNSPECIFIED. ) ;
#8987=FACE_OUTER_BOUND ( 'NONE', #10441, .T. ) ;
#8988=CARTESIAN_POINT ( 'NONE',  ( 2.789999999999999147, -9.999777909379854890, -11.07980565117290794 ) ) ;
#8991=CARTESIAN_POINT ( 'NONE',  ( 1.039999999999999147, -17.39253030560838198, -4.458161950358684678 ) ) ;
#9000=ORIENTED_EDGE ( 'NONE', *, *, #1194, .T. ) ;
#9001=CARTESIAN_POINT ( 'NONE',  ( 0.02531912748606271468, -5.229914364928256454, -13.68080036884353845 ) ) ;
#9005=AXIS2_PLACEMENT_3D ( 'NONE', #4748, #6046, #14115 ) ;
#9013=CARTESIAN_POINT ( 'NONE',  ( 0.6549552265645784965, 16.44225436089927683, 5.086950209440548321 ) ) ;
#9021=CARTESIAN_POINT ( 'NONE',  ( 0.000000000000000000, 13.87420763704361626, 1.948757464274225137 ) ) ;
#9026=EDGE_LOOP ( 'NONE', ( #4736, #308, #4974, #5991, #12502, #14574 ) ) ;
#9030=ORIENTED_EDGE ( 'NONE', *, *, #3701, .F. ) ;
#9035=CARTESIAN_POINT ( 'NONE',  ( 0.008751532933531189218, -13.40591150985895297, -5.214906618939850524 ) ) ;
#9037=CIRCLE ( 'NONE', #6583, 2.524999999999998579 ) ;
#9040=MANIFOLD_SOLID_BREP ( 'Bore', #1082 ) ;
#9042=ORIENTED_EDGE ( 'NONE', *, *, #3186, .T. ) ;
#9044=CIRCLE ( 'NONE', #1184, 2.524999999999999467 ) ;
#9051=AXIS2_PLACEMENT_3D ( 'NONE', #1806, #6580, #12560 ) ;
#9054=B_SPLINE_CURVE_WITH_KNOTS ( 'NONE', 3,
 ( #8937, #1797, #6482, #13628 ),
 .UNSPECIFIED., .F., .F.,
 ( 4, 4 ),
 ( 1.988537750524637048E-07, 0.0006916721208754034915 ),
 .UNSPECIFIED. ) ;
#9068=CARTESIAN_POINT ( 'NONE',  ( 0.04999671820202215150, 5.264737421541719975, -13.99876742897254012 ) ) ;
#9069=CARTESIAN_POINT ( 'NONE',  ( 2.789999999999999147, -5.249430348645663713, -12.98979500319699731 ) ) ;
#9072=CARTESIAN_POINT ( 'NONE',  ( 1.749999999999999778, -4.835383649608351320, -17.29145405592693763 ) ) ;
#9084=AXIS2_PLACEMENT_3D ( 'NONE', #1450, #14589, #5157 ) ;
#9085=CARTESIAN_POINT ( 'NONE',  ( 2.764680872513937349, -13.68080036884344963, -5.229914364928496262 ) ) ;
#9086=( NAMED_UNIT ( * ) PLANE_ANGLE_UNIT ( ) SI_UNIT ( $, .RADIAN. ) );
#9087=ADVANCED_FACE ( 'NONE', ( #1081 ), #2876, .T. ) ;
#9093=B_SPLINE_CURVE_WITH_KNOTS ( 'NONE', 3,
 ( #5634, #12604, #10379, #9001 ),
 .UNSPECIFIED., .F., .F.,
 ( 4, 4 ),
 ( 0.005123742438166226966, 0.005814376014856854902 ),
 .UNSPECIFIED. ) ;
#9097=ADVANCED_FACE ( 'NONE', ( #1009 ), #14710, .T. ) ;
#9099=ORIENTED_EDGE ( 'NONE', *, *, #12674, .T. ) ;
#9126=FACE_OUTER_BOUND ( 'NONE', #10259, .T. ) ;
#9129=CYLINDRICAL_SURFACE ( 'NONE', #14711, 2.524999999999998579 ) ;
#9134=DIRECTION ( 'NONE',  ( 0.000000000000000000, 0.000000000000000000, 1.000000000000000000 ) ) ;
#9138=CARTESIAN_POINT ( 'NONE',  ( 0.02531912748464674665, 5.229914364928542447, -13.68080036884343009 ) ) ;
#9143=DIRECTION ( 'NONE',  ( 0.000000000000000000, 0.000000000000000000, 1.000000000000000000 ) ) ;
#9147=ORIENTED_EDGE ( 'NONE', *, *, #5784, .T. ) ;
#9157=DIRECTION ( 'NONE',  ( -1.000000000000000000, -0.000000000000000000, -0.000000000000000000 ) ) ;
#9166=CARTESIAN_POINT ( 'NONE',  ( 1.039999999999997149, 17.39253030560841751, -4.458161950358562997 ) ) ;
#9176=VERTEX_POINT ( 'NONE', #2387 ) ;
#9181=ORIENTED_EDGE ( 'NONE', *, *, #14063, .F. ) ;
#9184=CARTESIAN_POINT ( 'NONE',  ( 0.09203966225861176520, 2.583706482362034151, 15.03709480088672734 ) ) ;
#9185=ORIENTED_EDGE ( 'NONE', *, *, #12019, .T. ) ;
#9188=VERTEX_POINT ( 'NONE', #2616 ) ;
#9199=LINE ( 'NONE', #6962, #2933 ) ;
#9201=VERTEX_POINT ( 'NONE', #10764 ) ;
#9213=CARTESIAN_POINT ( 'NONE',  ( 0.2076373605413179835, 5.278564329441211456, -14.94126095370955731 ) ) ;
#9214=DIRECTION ( 'NONE',  ( -1.000000000000000000, -0.000000000000000000, -0.000000000000000000 ) ) ;
#9220=CIRCLE ( 'NONE', #2344, 14.01039946648073986 ) ;
#9222=DIRECTION ( 'NONE',  ( 0.000000000000000000, 0.000000000000000000, 1.000000000000000000 ) ) ;
#9224=EDGE_CURVE ( 'NONE', #11407, #13089, #53, .T. ) ;
#9225=ORIENTED_EDGE ( 'NONE', *, *, #13904, .T. ) ;
#9229=ORIENTED_EDGE ( 'NONE', *, *, #7210, .T. ) ;
#9236=EDGE_CURVE ( 'NONE', #11663, #2567, #4301, .T. ) ;
#9243=B_SPLINE_CURVE_WITH_KNOTS ( 'NONE', 3,
 ( #6292, #11201, #1756, #676 ),
 .UNSPECIFIED., .F., .F.,
 ( 4, 4 ),
 ( 1.988537749986050620E-07, 0.0002742066915197750193 ),
 .UNSPECIFIED. ) ;
#9244=CARTESIAN_POINT ( 'NONE',  ( 0.02531912748256377743, 14.46287784598617421, -2.311161484776606212 ) ) ;
#9245=EDGE_CURVE ( 'NONE', #14739, #8589, #7613, .T. ) ;
#9249=AXIS2_PLACEMENT_3D ( 'NONE', #9940, #2792, #11165 ) ;
#9251=CARTESIAN_POINT ( 'NONE',  ( 2.764680872513208598, 11.36963888406700285, -9.232963481057645083 ) ) ;
#9252=ORIENTED_EDGE ( 'NONE', *, *, #6365, .T. ) ;
#9258=CARTESIAN_POINT ( 'NONE',  ( 2.764680872515352661, 9.232963481057920418, -11.36963888406677725 ) ) ;
#9259=CARTESIAN_POINT ( 'NONE',  ( 2.789999999999999147, -11.04103753892277417, 8.624777288397760699 ) ) ;
#9262=VECTOR ( 'NONE', #14812, 1000.000000000000000 ) ;
#9267=AXIS2_PLACEMENT_3D ( 'NONE', #11213, #11292, #2144 ) ;
#9270=CARTESIAN_POINT ( 'NONE',  ( 0.000000000000000000, 5.249430348645932831, -12.98979500319689251 ) ) ;
#9272=ADVANCED_FACE ( 'NONE', ( #13361 ), #4111, .T. ) ;
#9278=CARTESIAN_POINT ( 'NONE',  ( 0.007327532539343941352, 14.24942254254686169, -2.217238903388591087 ) ) ;
#9280=AXIS2_PLACEMENT_3D ( 'NONE', #14717, #11315, #1718 ) ;
#9285=DIRECTION ( 'NONE',  ( -1.000000000000000000, -0.000000000000000000, -0.000000000000000000 ) ) ;
#9287=EDGE_CURVE ( 'NONE', #8287, #8724, #8035, .T. ) ;
#9291=CARTESIAN_POINT ( 'NONE',  ( 0.04925989934398850717, -13.98927362834336918, 5.263697681271511719 ) ) ;
#9296=CARTESIAN_POINT ( 'NONE',  ( 0.09203962824862059466, 9.756102650610241511, 11.73065272960066707 ) ) ;
#9304=EDGE_CURVE ( 'NONE', #7716, #14810, #4152, .T. ) ;
#9319=CARTESIAN_POINT ( 'NONE',  ( 1.749999999999999778, -4.835383649608351320, -17.29145405592693763 ) ) ;
#9325=ORIENTED_EDGE ( 'NONE', *, *, #11542, .T. ) ;
#9328=ORIENTED_EDGE ( 'NONE', *, *, #5091, .F. ) ;
#9329=EDGE_LOOP ( 'NONE', ( #3868, #3002, #12735, #2533 ) ) ;
#9334=CARTESIAN_POINT ( 'NONE',  ( 2.508169608347904145, 15.25429862889489208, -5.259531939870039530 ) ) ;
#9336=EDGE_CURVE ( 'NONE', #3644, #1400, #10906, .T. ) ;
#9344=CARTESIAN_POINT ( 'NONE',  ( 2.789999999999999147, -15.47981323787947794, -1.080949580976661932E-13 ) ) ;
#9350=EDGE_LOOP ( 'NONE', ( #6254, #9328, #14449, #6702, #11867, #13284 ) ) ;
#9353=CARTESIAN_POINT ( 'NONE',  ( 0.000000000000000000, 11.04103753892283635, -8.624777288397693198 ) ) ;
#9357=VERTEX_POINT ( 'NONE', #11125 ) ;
#9358=EDGE_LOOP ( 'NONE', ( #12894, #8178, #9252, #9042, #6395, #7831 ) ) ;
#9362=CARTESIAN_POINT ( 'NONE',  ( 0.000000000000000000, 11.04103753892283635, -8.624777288397693198 ) ) ;
#9365=ADVANCED_FACE ( 'NONE', ( #599 ), #5317, .T. ) ;
#9375=DIRECTION ( 'NONE',  ( -1.000000000000000000, -0.000000000000000000, -0.000000000000000000 ) ) ;
#9377=CARTESIAN_POINT ( 'NONE',  ( 0.5537796329733301048, -5.139875429511743476, -16.15122426806993872 ) ) ;
#9381=CARTESIAN_POINT ( 'NONE',  ( 2.246812931352481169, 12.54666350726123447, 11.42270873787296992 ) ) ;
#9392=CIRCLE ( 'NONE', #5490, 2.524999999999999467 ) ;
#9396=DIRECTION ( 'NONE',  ( -1.000000000000000000, -0.000000000000000000, -0.000000000000000000 ) ) ;
#9399=EDGE_LOOP ( 'NONE', ( #8056, #1716, #5192, #4952, #4653, #3864 ) ) ;
#9401=CARTESIAN_POINT ( 'NONE',  ( 0.1920563539683071974, 2.883512197589228165, -15.58455734132163251 ) ) ;
#9403=ORIENTED_EDGE ( 'NONE', *, *, #386, .T. ) ;
#9409=DIRECTION ( 'NONE',  ( -1.000000000000000000, 0.000000000000000000, 0.000000000000000000 ) ) ;
#9410=EDGE_CURVE ( 'NONE', #7166, #13214, #12906, .T. ) ;
#9420=VECTOR ( 'NONE', #7542, 1000.000000000000000 ) ;
#9426=CARTESIAN_POINT ( 'NONE',  ( 1.749999999999999778, 12.83329210556849453, -12.55714665599973578 ) ) ;
#9430=CARTESIAN_POINT ( 'NONE',  ( 0.007327564474061625845, 11.23174270417341880, -9.044896821682087307 ) ) ;
#9438=DIRECTION ( 'NONE',  ( -1.000000000000000000, -0.000000000000000000, -0.000000000000000000 ) ) ;
#9441=EDGE_LOOP ( 'NONE', ( #10557, #8725, #11525, #10656 ) ) ;
#9448=CARTESIAN_POINT ( 'NONE',  ( 2.764680872513208598, 11.36963888406700285, -9.232963481057645083 ) ) ;
#9451=CYLINDRICAL_SURFACE ( 'NONE', #4374, 2.524999999999999467 ) ;
#9452=CARTESIAN_POINT ( 'NONE',  ( 1.749999999999999778, -4.458161950358622505, 17.39253030560840330 ) ) ;
#9453=ADVANCED_FACE ( 'NONE', ( #12523 ), #4616, .T. ) ;
#9458=EDGE_CURVE ( 'NONE', #8188, #6679, #388, .T. ) ;
#9460=ADVANCED_FACE ( 'NONE', ( #11362 ), #3228, .T. ) ;
#9462=CARTESIAN_POINT ( 'NONE',  ( 0.000000000000000000, 0.000000000000000000, 0.000000000000000000 ) ) ;
#9466=ORIENTED_EDGE ( 'NONE', *, *, #14379, .F. ) ;
#9469=ORIENTED_EDGE ( 'NONE', *, *, #10826, .T. ) ;
#9474=DIRECTION ( 'NONE',  ( -1.000000000000000000, 0.000000000000000000, -0.000000000000000000 ) ) ;
#9477=ORIENTED_EDGE ( 'NONE', *, *, #8444, .T. ) ;
#9495=CARTESIAN_POINT ( 'NONE',  ( 0.007349531976027940186, -2.217353748342030695, 14.24968354755767663 ) ) ;
#9500=CARTESIAN_POINT ( 'NONE',  ( 0.000000000000000000, -11.04103753892277417, 8.624777288397769581 ) ) ;
#9503=FACE_OUTER_BOUND ( 'NONE', #11850, .T. ) ;
#9504=CARTESIAN_POINT ( 'NONE',  ( 0.000000000000000000, 8.624777288397959651, -11.04103753892262674 ) ) ;
#9510=DIRECTION ( 'NONE',  ( -1.000000000000000000, -0.000000000000000000, -0.000000000000000000 ) ) ;
#9513=CARTESIAN_POINT ( 'NONE',  ( 1.039999999999996927, 4.835383649608473000, 17.29145405592690565 ) ) ;
#9522=DIRECTION ( 'NONE',  ( 0.000000000000000000, 0.000000000000000000, 1.000000000000000000 ) ) ;
#9529=VERTEX_POINT ( 'NONE', #7133 ) ;
#9535=CARTESIAN_POINT ( 'NONE',  ( 0.5537796532149688034, -3.624349476775314383, 16.55730827443879605 ) ) ;
#9547=ORIENTED_EDGE ( 'NONE', *, *, #12674, .F. ) ;
#9554=CARTESIAN_POINT ( 'NONE',  ( 2.789999999999999147, 15.47981323787947794, 0.000000000000000000 ) ) ;
#9555=CARTESIAN_POINT ( 'NONE',  ( 2.582362678678089107, -15.57879356040261243, -2.899259574942910866 ) ) ;
#9556=AXIS2_PLACEMENT_3D ( 'NONE', #7863, #12470, #7782 ) ;
#9567=CARTESIAN_POINT ( 'NONE',  ( 0.4522159468065701238, -12.42068120944072795, -11.13074453164216138 ) ) ;
#9571=CARTESIAN_POINT ( 'NONE',  ( 2.790000000000060876, 14.05326139264727736, 2.096282088614815908 ) ) ;
#9579=FACE_OUTER_BOUND ( 'NONE', #11348, .T. ) ;
#9583=ORIENTED_EDGE ( 'NONE', *, *, #5443, .F. ) ;
#9588=DIRECTION ( 'NONE',  ( -1.000000000000000000, 0.000000000000000000, -0.000000000000000000 ) ) ;
#9595=VERTEX_POINT ( 'NONE', #11655 ) ;
#9597=CARTESIAN_POINT ( 'NONE',  ( 0.4522159468065704013, 11.13074453164220579, -12.42068120944069420 ) ) ;
#9602=VERTEX_POINT ( 'NONE', #14277 ) ;
#9605=CARTESIAN_POINT ( 'NONE',  ( 2.790000000000010694, 14.05347802000167512, -2.096460570596210271 ) ) ;
#9606=FACE_OUTER_BOUND ( 'NONE', #7130, .T. ) ;
#9610=ORIENTED_EDGE ( 'NONE', *, *, #4222, .T. ) ;
#9623=AXIS2_PLACEMENT_3D ( 'NONE', #7506, #10806, #1579 ) ;
#9630=CARTESIAN_POINT ( 'NONE',  ( 2.789999999999999147, 14.46287784598617421, -2.311161484776606212 ) ) ;
#9633=CARTESIAN_POINT ( 'NONE',  ( 0.07473575470096514850, 11.74839219818087521, 9.749517823374048930 ) ) ;
#9634=EDGE_CURVE ( 'NONE', #3142, #4933, #13193, .T. ) ;
#9636=VERTEX_POINT ( 'NONE', #10960 ) ;
#9640=DIRECTION ( 'NONE',  ( 1.000000000000000000, 0.000000000000000000, 0.000000000000000000 ) ) ;
#9641=CARTESIAN_POINT ( 'NONE',  ( 2.789999999999999147, 5.249430348645936384, -12.98979500319688718 ) ) ;
#9646=CARTESIAN_POINT ( 'NONE',  ( 2.789999999999999147, -13.40591150984231916, 7.739906618939660810 ) ) ;
#9669=ORIENTED_EDGE ( 'NONE', *, *, #13116, .F. ) ;
#9670=VECTOR ( 'NONE', #9474, 1000.000000000000000 ) ;
#9672=CARTESIAN_POINT ( 'NONE',  ( 1.749999999999999778, -12.55714665599996138, 12.83329210556827249 ) ) ;
#9675=CARTESIAN_POINT ( 'NONE',  ( 1.394999999999999574, -12.83329210556840572, 12.55714665599982993 ) ) ;
#9679=CARTESIAN_POINT ( 'NONE',  ( 0.02531912748631555063, 2.311161484776756758, -14.46287784598614756 ) ) ;
#9684=CARTESIAN_POINT ( 'NONE',  ( -6.115811008765337794E-14, -2.096282088614671579, -14.05326139264730045 ) ) ;
#9693=TOROIDAL_SURFACE ( 'NONE', #12139, 14.01039946648073986, 8.000000000000000000 ) ;
#9698=DIRECTION ( 'NONE',  ( 0.000000000000000000, 6.870191984066563922E-16, -1.000000000000000000 ) ) ;
#9706=FACE_OUTER_BOUND ( 'NONE', #5655, .T. ) ;
#9713=CARTESIAN_POINT ( 'NONE',  ( 0.2818302809372413287, 12.18203740414281278, -10.58084377126610498 ) ) ;
#9722=DIRECTION ( 'NONE',  ( -1.000000000000000000, 0.000000000000000000, -0.000000000000000000 ) ) ;
#9744=CARTESIAN_POINT ( 'NONE',  ( 2.646101151981377075, 14.59528211759998406, 5.279841123860917307 ) ) ;
#9755=ORIENTED_EDGE ( 'NONE', *, *, #2735, .T. ) ;
#9756=AXIS2_PLACEMENT_3D ( 'NONE', #10658, #9510, #8351 ) ;
#9758=CARTESIAN_POINT ( 'NONE',  ( 1.885839517048297775, 17.20101185193998816, -4.239993951493249646 ) ) ;
#9759=LINE ( 'NONE', #9675, #2353 ) ;
#9765=CARTESIAN_POINT ( 'NONE',  ( 0.000000000000000000, 0.000000000000000000, 0.000000000000000000 ) ) ;
#9768=EDGE_CURVE ( 'NONE', #1826, #7052, #12698, .T. ) ;
#9777=EDGE_CURVE ( 'NONE', #5623, #2515, #14888, .T. ) ;
#9778=( LENGTH_UNIT ( ) NAMED_UNIT ( * ) SI_UNIT ( .MILLI., .METRE. ) );
#9779=ORIENTED_EDGE ( 'NONE', *, *, #8584, .F. ) ;
#9781=CARTESIAN_POINT ( 'NONE',  ( -6.202591138825049061E-14, 8.842064619038524143, 11.12234047011193283 ) ) ;
#9782=CARTESIAN_POINT ( 'NONE',  ( 2.789999999999999147, 1.948757464274366136, -13.87420763704359139 ) ) ;
#9786=PRODUCT_DEFINITION_CONTEXT ( 'detailed design', #7547, 'design' ) ;
#9788=B_SPLINE_CURVE_WITH_KNOTS ( 'NONE', 3,
 ( #10252, #14954, #4651, #9251 ),
 .UNSPECIFIED., .F., .F.,
 ( 4, 4 ),
 ( 0.005123695899043906321, 0.005814329666474870977 ),
 .UNSPECIFIED. ) ;
#9795=AXIS2_PLACEMENT_3D ( 'NONE', #1750, #7825, #10053 ) ;
#9810=CARTESIAN_POINT ( 'NONE',  ( 2.764680872515354881, -13.68080036884352246, 5.229914364928304416 ) ) ;
#9812=CYLINDRICAL_SURFACE ( 'NONE', #8514, 8.400000000000000355 ) ;
#9818=CARTESIAN_POINT ( 'NONE',  ( 0.000000000000000000, 12.98979500319701685, -5.249430348645618416 ) ) ;
#9822=SHAPE_DEFINITION_REPRESENTATION ( #256, #4172 ) ;
#9830=CARTESIAN_POINT ( 'NONE',  ( 1.394999999999998685, 4.458161950358745074, -17.39253030560836777 ) ) ;
#9844=CARTESIAN_POINT ( 'NONE',  ( 2.789999999999999147, 1.621424371464993087E-13, -12.95481323787947936 ) ) ;
#9854=ORIENTED_EDGE ( 'NONE', *, *, #7297, .F. ) ;
#9856=ADVANCED_FACE ( 'NONE', ( #14813 ), #14744, .F. ) ;
#9858=CARTESIAN_POINT ( 'NONE',  ( 1.749999999999999778, 12.83329210556831690, 12.55714665599991875 ) ) ;
#9870=AXIS2_PLACEMENT_3D ( 'NONE', #9646, #11945, #6419 ) ;
#9872=EDGE_CURVE ( 'NONE', #13954, #1071, #10263, .T. ) ;
#9877=CARTESIAN_POINT ( 'NONE',  ( 0.000000000000000000, 0.000000000000000000, 0.000000000000000000 ) ) ;
#9888=CARTESIAN_POINT ( 'NONE',  ( 2.715264182578264851, 5.299647274067300629, -14.31752701692930962 ) ) ;
#9889=CYLINDRICAL_SURFACE ( 'NONE', #3677, 17.95481323787947403 ) ;
#9891=ORIENTED_EDGE ( 'NONE', *, *, #8428, .T. ) ;
#9903=DIRECTION ( 'NONE',  ( 1.000000000000000000, -0.000000000000000000, -0.000000000000000000 ) ) ;
#9915=ORIENTED_EDGE ( 'NONE', *, *, #12938, .T. ) ;
#9916=ORIENTED_EDGE ( 'NONE', *, *, #10840, .T. ) ;
#9917=ORIENTED_EDGE ( 'NONE', *, *, #3737, .F. ) ;
#9924=VECTOR ( 'NONE', #1073, 1000.000000000000000 ) ;
#9925=UNCERTAINTY_MEASURE_WITH_UNIT (LENGTH_MEASURE( 1.000000000000000082E-05 ), #4169, 'distance_accuracy_value', 'NONE');
#9928=ORIENTED_EDGE ( 'NONE', *, *, #4776, .F. ) ;
#9940=CARTESIAN_POINT ( 'NONE',  ( 1.749999999999999778, 0.000000000000000000, 0.000000000000000000 ) ) ;
#9941=CARTESIAN_POINT ( 'NONE',  ( 2.246812931352479392, -12.54666350726115631, -11.42270873787306229 ) ) ;
#9944=CARTESIAN_POINT ( 'NONE',  ( 0.000000000000000000, 5.249430348645932831, -12.98979500319689251 ) ) ;
#9952=CARTESIAN_POINT ( 'NONE',  ( 2.789999999999999147, -1.948757464274075479, -13.87420763704363225 ) ) ;
#9985=ORIENTED_EDGE ( 'NONE', *, *, #12144, .T. ) ;
#9986=EDGE_CURVE ( 'NONE', #4412, #6955, #1688, .T. ) ;
#9988=DIRECTION ( 'NONE',  ( 0.000000000000000000, 0.000000000000000000, 1.000000000000000000 ) ) ;
#9993=CARTESIAN_POINT ( 'NONE',  ( 2.010451923687323283, 11.98750039041494198, 12.70439593876664652 ) ) ;
#9998=CARTESIAN_POINT ( 'NONE',  ( 2.789999999999999147, 15.47981323787947794, 0.000000000000000000 ) ) ;
#10003=VERTEX_POINT ( 'NONE', #15117 ) ;
#10005=CARTESIAN_POINT ( 'NONE',  ( 2.782672467460656218, -14.24942254254687946, -2.217238903388711435 ) ) ;
#10014=ORIENTED_EDGE ( 'NONE', *, *, #1986, .T. ) ;
#10017=CARTESIAN_POINT ( 'NONE',  ( 0.3603712044621530941, 15.53862542373106415, 5.230001598524659734 ) ) ;
#10022=CIRCLE ( 'NONE', #4877, 2.524999999999998135 ) ;
#10028=DIRECTION ( 'NONE',  ( -1.000000000000000000, 0.000000000000000000, -0.000000000000000000 ) ) ;
#10040=ORIENTED_EDGE ( 'NONE', *, *, #3701, .T. ) ;
#10051=CYLINDRICAL_SURFACE ( 'NONE', #7732, 8.399999999999998579 ) ;
#10053=DIRECTION ( 'NONE',  ( 0.000000000000000000, 0.000000000000000000, 1.000000000000000000 ) ) ;
#10054=DIRECTION ( 'NONE',  ( 0.000000000000000000, 0.000000000000000000, -1.000000000000000000 ) ) ;
#10057=VERTEX_POINT ( 'NONE', #4738 ) ;
#10058=DIRECTION ( 'NONE',  ( -1.000000000000000000, -0.000000000000000000, 0.000000000000000000 ) ) ;
#10060=DIRECTION ( 'NONE',  ( -1.000000000000000000, -0.000000000000000000, -0.000000000000000000 ) ) ;
#10062=CARTESIAN_POINT ( 'NONE',  ( 2.789999999999999147, -7.739906618939614624, -13.40591150984234581 ) ) ;
#10066=DIRECTION ( 'NONE',  ( -1.000000000000000000, -0.000000000000000000, -0.000000000000000000 ) ) ;
#10077=ORIENTED_EDGE ( 'NONE', *, *, #13691, .F. ) ;
#10080=VERTEX_POINT ( 'NONE', #1264 ) ;
#10087=VERTEX_POINT ( 'NONE', #12018 ) ;
#10093=ORIENTED_EDGE ( 'NONE', *, *, #14484, .T. ) ;
#10096=DIRECTION ( 'NONE',  ( -1.000000000000000000, 0.000000000000000000, 0.000000000000000000 ) ) ;
#10099=CYLINDRICAL_SURFACE ( 'NONE', #15192, 8.400000000000000355 ) ;
#10104=CARTESIAN_POINT ( 'NONE',  ( 2.764680872513207266, -9.232963481057685939, -11.36963888406697087 ) ) ;
#10108=ORIENTED_EDGE ( 'NONE', *, *, #8414, .F. ) ;
#10119=CARTESIAN_POINT ( 'NONE',  ( 2.764680872513207266, -9.232963481057685939, -11.36963888406697087 ) ) ;
#10125=ORIENTED_EDGE ( 'NONE', *, *, #6440, .F. ) ;
#10126=CARTESIAN_POINT ( 'NONE',  ( 2.789999999999999147, 5.229914364928542447, -13.68080036884343009 ) ) ;
#10128=TOROIDAL_SURFACE ( 'NONE', #3291, 14.01039946648074341, 8.000000000000000000 ) ;
#10137=ORIENTED_EDGE ( 'NONE', *, *, #4204, .F. ) ;
#10141=CARTESIAN_POINT ( 'NONE',  ( 2.782672467460654442, 2.217238903388760285, -14.24942254254687057 ) ) ;
#10151=ORIENTED_EDGE ( 'NONE', *, *, #13139, .T. ) ;
#10158=ADVANCED_FACE ( 'NONE', ( #5205 ), #10941, .T. ) ;
#10159=CYLINDRICAL_SURFACE ( 'NONE', #12257, 17.95481323787947403 ) ;
#10162=DIRECTION ( 'NONE',  ( -1.000000000000000000, 0.000000000000000000, -0.000000000000000000 ) ) ;
#10170=DIRECTION ( 'NONE',  ( -1.000000000000000000, -0.000000000000000000, -0.000000000000000000 ) ) ;
#10171=CARTESIAN_POINT ( 'NONE',  ( 1.749999999999999778, -17.29145405592692342, 4.835383649608411716 ) ) ;
#10175=CARTESIAN_POINT ( 'NONE',  ( 0.02531912748606271468, -5.229914364928256454, -13.68080036884353845 ) ) ;
#10180=TOROIDAL_SURFACE ( 'NONE', #11149, 14.01039946648073986, 8.000000000000000000 ) ;
#10200=AXIS2_PLACEMENT_3D ( 'NONE', #8482, #9722, #8712 ) ;
#10201=ORIENTED_EDGE ( 'NONE', *, *, #1121, .T. ) ;
#10202=CARTESIAN_POINT ( 'NONE',  ( 8.000000000000000000, 0.000000000000000000, 0.000000000000000000 ) ) ;
#10204=CARTESIAN_POINT ( 'NONE',  ( 2.782650494170369804, -5.204557061642381299, 13.44926448535264463 ) ) ;
#10207=FACE_OUTER_BOUND ( 'NONE', #14846, .T. ) ;
#10212=CARTESIAN_POINT ( 'NONE',  ( 2.781248467067199748, -13.40591150984217705, -5.214906618939849636 ) ) ;
#10214=CARTESIAN_POINT ( 'NONE',  ( 2.010451919658892361, -16.99607982911243909, 4.029281904976570239 ) ) ;
#10215=DIRECTION ( 'NONE',  ( 1.000000000000000000, -0.000000000000000000, -0.000000000000000000 ) ) ;
#10218=EDGE_CURVE ( 'NONE', #1632, #7996, #10022, .T. ) ;
#10227=ORIENTED_EDGE ( 'NONE', *, *, #6171, .F. ) ;
#10231=ADVANCED_FACE ( 'NONE', ( #4194 ), #10099, .T. ) ;
#10232=CARTESIAN_POINT ( 'NONE',  ( 2.010451923687323283, -12.70439593876669271, 11.98750039041489224 ) ) ;
#10239=AXIS2_PLACEMENT_3D ( 'NONE', #12522, #10066, #13895 ) ;
#10247=CARTESIAN_POINT ( 'NONE',  ( 2.764680872515352661, -2.311161484776655950, 14.46287784598616355 ) ) ;
#10251=CARTESIAN_POINT ( 'NONE',  ( 0.000000000000000000, -7.739906618939802918, 13.40591150984224100 ) ) ;
#10252=CARTESIAN_POINT ( 'NONE',  ( 2.789999999999999147, 11.04103753892283635, -8.624777288397684316 ) ) ;
#10259=EDGE_LOOP ( 'NONE', ( #14512, #11772, #12228, #12444, #1205, #13419, #2005 ) ) ;
#10263=CIRCLE ( 'NONE', #4377, 14.01039946648074341 ) ;
#10266=B_SPLINE_CURVE_WITH_KNOTS ( 'NONE', 3,
 ( #7226, #9605, #3531, #4860 ),
 .UNSPECIFIED., .F., .F.,
 ( 4, 4 ),
 ( 0.005123713096549374624, 0.005814346476695759873 ),
 .UNSPECIFIED. ) ;
#10268=VERTEX_POINT ( 'NONE', #12322 ) ;
#10278=DIRECTION ( 'NONE',  ( -1.000000000000000000, -0.000000000000000000, -0.000000000000000000 ) ) ;
#10283=CARTESIAN_POINT ( 'NONE',  ( 0.02531912748286561932, 13.68080036884348516, 5.229914364928400339 ) ) ;
#10285=VECTOR ( 'NONE', #10333, 1000.000000000000000 ) ;
#10291=CARTESIAN_POINT ( 'NONE',  ( 0.5431871499410856341, 5.154374911959137329, -16.16568790143436019 ) ) ;
#10295=CARTESIAN_POINT ( 'NONE',  ( 0.000000000000000000, -13.87420763704362869, 1.948757464274129214 ) ) ;
#10297=LINE ( 'NONE', #4233, #13614 ) ;
#10304=CARTESIAN_POINT ( 'NONE',  ( 2.790000000000060876, -2.096282088614865646, 14.05326139264726848 ) ) ;
#10315=CARTESIAN_POINT ( 'NONE',  ( 0.7686372158811271005, -11.98841295390588435, -12.71987259277447180 ) ) ;
#10316=CARTESIAN_POINT ( 'NONE',  ( 0.02531912748631468327, -14.46287784598615644, -2.311161484776706576 ) ) ;
#10325=CARTESIAN_POINT ( 'NONE',  ( 2.789999999999999147, 11.07980565117280314, -9.999777909379972129 ) ) ;
#10333=DIRECTION ( 'NONE',  ( -1.000000000000000000, 0.000000000000000000, 0.000000000000000000 ) ) ;
#10347=ORIENTED_EDGE ( 'NONE', *, *, #4118, .F. ) ;
#10358=CARTESIAN_POINT ( 'NONE',  ( 8.000000000000000000, 0.000000000000000000, 0.000000000000000000 ) ) ;
#10373=EDGE_CURVE ( 'NONE', #11075, #960, #8085, .T. ) ;
#10376=EDGE_LOOP ( 'NONE', ( #13286, #4686, #584, #12146, #14551, #2535 ) ) ;
#10379=CARTESIAN_POINT ( 'NONE',  ( 0.007349505829628827543, -5.204557061642193005, -13.44926448535271568 ) ) ;
#10391=DIRECTION ( 'NONE',  ( -1.000000000000000000, -0.000000000000000000, -0.000000000000000000 ) ) ;
#10397=ORIENTED_EDGE ( 'NONE', *, *, #3175, .F. ) ;
#10398=CARTESIAN_POINT ( 'NONE',  ( 1.749999999999999778, -12.55714665599977842, -12.83329210556845190 ) ) ;
#10402=CARTESIAN_POINT ( 'NONE',  ( 2.361335444912569859, -15.76776810790841310, 5.200734291367588469 ) ) ;
#10407=AXIS2_PLACEMENT_3D ( 'NONE', #4573, #4145, #13511 ) ;
#10408=CARTESIAN_POINT ( 'NONE',  ( 2.789999999999999147, 13.40591150984237245, -7.739906618939567551 ) ) ;
#10409=ORIENTED_EDGE ( 'NONE', *, *, #9410, .T. ) ;
#10411=ORIENTED_EDGE ( 'NONE', *, *, #6548, .T. ) ;
#10416=EDGE_CURVE ( 'NONE', #3069, #2383, #13611, .T. ) ;
#10423=ADVANCED_FACE ( 'NONE', ( #9606 ), #2618, .T. ) ;
#10425=EDGE_LOOP ( 'NONE', ( #6522, #5375, #6484, #9181, #5941, #2130 ) ) ;
#10434=VECTOR ( 'NONE', #6336, 1000.000000000000000 ) ;
#10440=CARTESIAN_POINT ( 'NONE',  ( 2.764680872515353993, -5.229914364928256454, -13.68080036884353845 ) ) ;
#10441=EDGE_LOOP ( 'NONE', ( #6112, #9669, #9030, #3218, #7510, #5290 ) ) ;
#10442=CARTESIAN_POINT ( 'NONE',  ( 2.764680872513682885, -14.46287784598619020, 2.311161484776505404 ) ) ;
#10443=DIRECTION ( 'NONE',  ( 0.000000000000000000, 0.000000000000000000, 1.000000000000000000 ) ) ;
#10452=DIRECTION ( 'NONE',  ( -1.000000000000000000, 0.000000000000000000, -0.000000000000000000 ) ) ;
#10454=EDGE_CURVE ( 'NONE', #10268, #4197, #11747, .T. ) ;
#10458=EDGE_LOOP ( 'NONE', ( #15216, #946, #15153, #2468 ) ) ;
#10459=CARTESIAN_POINT ( 'NONE',  ( 2.236220312281012035, -12.52687487503427022, 11.41743294611070247 ) ) ;
#10471=FACE_OUTER_BOUND ( 'NONE', #6871, .T. ) ;
#10480=AXIS2_PLACEMENT_3D ( 'NONE', #1132, #9285, #10584 ) ;
#10486=EDGE_CURVE ( 'NONE', #12007, #11663, #343, .T. ) ;
#10494=CARTESIAN_POINT ( 'NONE',  ( 0.1438988480186108865, -14.59528211759996630, 5.279841123860814278 ) ) ;
#10495=( GEOMETRIC_REPRESENTATION_CONTEXT ( 3 ) GLOBAL_UNCERTAINTY_ASSIGNED_CONTEXT ( ( #5708 ) ) GLOBAL_UNIT_ASSIGNED_CONTEXT ( ( #13836, #9086, #2307 ) ) REPRESENTATION_CONTEXT ( 'NONE', 'WORKASPACE' ) );
#10501=CARTESIAN_POINT ( 'NONE',  ( 0.02531912748679390063, 9.232963481057920418, -11.36963888406677725 ) ) ;
#10510=ORIENTED_EDGE ( 'NONE', *, *, #12845, .F. ) ;
#10518=EDGE_LOOP ( 'NONE', ( #1614, #14415, #1169, #4914, #2425, #2023, #6851 ) ) ;
#10520=CARTESIAN_POINT ( 'NONE',  ( 2.789999999999999147, 11.04103753892283635, -8.624777288397684316 ) ) ;
#10526=LINE ( 'NONE', #13373, #5588 ) ;
#10534=AXIS2_PLACEMENT_3D ( 'NONE', #10598, #12886, #14130 ) ;
#10535=CIRCLE ( 'NONE', #11014, 2.524999999999999023 ) ;
#10536=AXIS2_PLACEMENT_3D ( 'NONE', #2574, #7268, #13467 ) ;
#10538=EDGE_LOOP ( 'NONE', ( #2181, #4718, #3070, #12804 ) ) ;
#10543=CARTESIAN_POINT ( 'NONE',  ( 0.8341307846263376069, -16.87476769693377321, 4.976600677180410770 ) ) ;
#10555=EDGE_CURVE ( 'NONE', #13089, #10675, #8906, .T. ) ;
#10557=ORIENTED_EDGE ( 'NONE', *, *, #2847, .T. ) ;
#10559=B_SPLINE_CURVE_WITH_KNOTS ( 'NONE', 3,
 ( #11231, #4175, #9781, #14480 ),
 .UNSPECIFIED., .F., .F.,
 ( 4, 4 ),
 ( 2.451234579310871045E-07, 0.0006917187676826522767 ),
 .UNSPECIFIED. ) ;
#10561=LINE ( 'NONE', #77, #11887 ) ;
#10569=CARTESIAN_POINT ( 'NONE',  ( 0.000000000000000000, 1.621424371464993087E-13, -12.95481323787947936 ) ) ;
#10571=EDGE_CURVE ( 'NONE', #6770, #11883, #11554, .T. ) ;
#10573=CARTESIAN_POINT ( 'NONE',  ( 0.02531912748464587928, -5.229914364928447412, 13.68080036884346917 ) ) ;
#10577=DIRECTION ( 'NONE',  ( 0.000000000000000000, 0.000000000000000000, -1.000000000000000000 ) ) ;
#10579=CARTESIAN_POINT ( 'NONE',  ( 1.394999999999999574, 17.39253030560841751, -4.458161950358562109 ) ) ;
#10584=DIRECTION ( 'NONE',  ( 0.000000000000000000, 0.000000000000000000, 1.000000000000000000 ) ) ;
#10598=CARTESIAN_POINT ( 'NONE',  ( -5.209999999999999964, 0.000000000000000000, 0.000000000000000000 ) ) ;
#10599=EDGE_CURVE ( 'NONE', #3713, #3154, #3159, .T. ) ;
#10600=EDGE_CURVE ( 'NONE', #1772, #2773, #7915, .T. ) ;
#10609=DIRECTION ( 'NONE',  ( -1.000000000000000000, -0.000000000000000000, -0.000000000000000000 ) ) ;
#10616=B_SPLINE_CURVE_WITH_KNOTS ( 'NONE', 3,
 ( #5706, #10315, #15163, #8152, #6928, #11604, #1083, #4639 ),
 .UNSPECIFIED., .F., .F.,
 ( 4, 2, 2, 4 ),
 ( 4.663089536289470154E-07, 0.001898630414085403445, 0.002847712466651290599, 0.003796794519217177970 ),
 .UNSPECIFIED. ) ;
#10619=DIRECTION ( 'NONE',  ( -1.000000000000000000, -0.000000000000000000, -0.000000000000000000 ) ) ;
#10621=ADVANCED_FACE ( 'NONE', ( #6685 ), #11365, .F. ) ;
#10622=ORIENTED_EDGE ( 'NONE', *, *, #6937, .T. ) ;
#10628=EDGE_LOOP ( 'NONE', ( #2828, #5502, #5142, #12992 ) ) ;
#10629=CARTESIAN_POINT ( 'NONE',  ( 0.02531912748631424959, 14.46287784598617243, 2.311161484776605324 ) ) ;
#10636=ORIENTED_EDGE ( 'NONE', *, *, #14073, .F. ) ;
#10638=DIRECTION ( 'NONE',  ( -1.000000000000000000, -0.000000000000000000, -0.000000000000000000 ) ) ;
#10641=DIRECTION ( 'NONE',  ( -1.000000000000000000, -0.000000000000000000, 0.000000000000000000 ) ) ;
#10644=EDGE_CURVE ( 'NONE', #516, #8949, #7958, .T. ) ;
#10650=CARTESIAN_POINT ( 'NONE',  ( 0.000000000000000000, 1.948757464274177842, 13.87420763704361981 ) ) ;
#10656=ORIENTED_EDGE ( 'NONE', *, *, #9245, .T. ) ;
#10658=CARTESIAN_POINT ( 'NONE',  ( 8.000000000000000000, 0.000000000000000000, 0.000000000000000000 ) ) ;
#10666=FACE_OUTER_BOUND ( 'NONE', #14386, .T. ) ;
#10671=CARTESIAN_POINT ( 'NONE',  ( 1.039999999999996039, -12.83329210556840394, 12.55714665599982816 ) ) ;
#10675=VERTEX_POINT ( 'NONE', #9072 ) ;
#10676=B_SPLINE_CURVE_WITH_KNOTS ( 'NONE', 3,
 ( #1330, #6026, #9401, #12713, #15109, #5733, #4666, #171 ),
 .UNSPECIFIED., .F., .F.,
 ( 4, 2, 2, 4 ),
 ( 2.154797737796238865E-07, 0.001895231411415137677, 0.002842739377235819348, 0.003790247343056501236 ),
 .UNSPECIFIED. ) ;
#10685=ADVANCED_FACE ( 'NONE', ( #2002 ), #13676, .T. ) ;
#10690=CARTESIAN_POINT ( 'NONE',  ( 0.02531912748464761401, -2.311161484776455222, -14.46287784598619908 ) ) ;
#10700=CARTESIAN_POINT ( 'NONE',  ( 0.5431871499410859672, -16.16568790143438150, -5.154374911959082262 ) ) ;
#10713=AXIS2_PLACEMENT_3D ( 'NONE', #6179, #10861, #320 ) ;
#10718=ORIENTED_EDGE ( 'NONE', *, *, #12144, .F. ) ;
#10719=DIRECTION ( 'NONE',  ( 0.000000000000000000, 0.000000000000000000, 1.000000000000000000 ) ) ;
#10722=CARTESIAN_POINT ( 'NONE',  ( 0.007349557670559650827, 9.045126717605935340, -11.23191127083853935 ) ) ;
#10724=AXIS2_PLACEMENT_3D ( 'NONE', #6217, #10060, #3919 ) ;
#10730=DIRECTION ( 'NONE',  ( -1.000000000000000000, 0.000000000000000000, 0.000000000000000000 ) ) ;
#10731=CARTESIAN_POINT ( 'NONE',  ( 1.394999999999999574, -4.458161950358622505, 17.39253030560840330 ) ) ;
#10736=ORIENTED_EDGE ( 'NONE', *, *, #13498, .F. ) ;
#10745=CARTESIAN_POINT ( 'NONE',  ( 2.789999999999999147, 4.595504208220227760, -14.19996452731184178 ) ) ;
#10747=CYLINDRICAL_SURFACE ( 'NONE', #6451, 8.400000000000000355 ) ;
#10756=EDGE_LOOP ( 'NONE', ( #11303, #8317, #5773, #12125 ) ) ;
#10760=VERTEX_POINT ( 'NONE', #1220 ) ;
#10761=ORIENTED_EDGE ( 'NONE', *, *, #5076, .T. ) ;
#10764=CARTESIAN_POINT ( 'NONE',  ( 0.02531912748464761401, -2.311161484776455222, -14.46287784598619908 ) ) ;
#10765=ADVANCED_FACE ( 'NONE', ( #7061 ), #12963, .T. ) ;
#10771=ORIENTED_EDGE ( 'NONE', *, *, #13704, .T. ) ;
#10787=EDGE_CURVE ( 'NONE', #13045, #484, #4416, .T. ) ;
#10789=DIRECTION ( 'NONE',  ( 1.000000000000000000, 0.000000000000000000, 0.000000000000000000 ) ) ;
#10790=DIRECTION ( 'NONE',  ( 0.000000000000000000, 0.000000000000000000, 1.000000000000000000 ) ) ;
#10795=CARTESIAN_POINT ( 'NONE',  ( 0.02531912748679129854, 11.36963888406687317, 9.232963481057801403 ) ) ;
#10805=CARTESIAN_POINT ( 'NONE',  ( 0.000000000000000000, 0.000000000000000000, 0.000000000000000000 ) ) ;
#10806=DIRECTION ( 'NONE',  ( -1.000000000000000000, -0.000000000000000000, -0.000000000000000000 ) ) ;
#10807=CARTESIAN_POINT ( 'NONE',  ( 2.764680872513682441, -2.311161484776455222, -14.46287784598619908 ) ) ;
#10808=DIRECTION ( 'NONE',  ( -1.000000000000000000, -0.000000000000000000, -0.000000000000000000 ) ) ;
#10809=VERTEX_POINT ( 'NONE', #10816 ) ;
#10816=CARTESIAN_POINT ( 'NONE',  ( 1.749999999999999778, 12.55714665600005020, -12.83329210556818545 ) ) ;
#10820=FACE_OUTER_BOUND ( 'NONE', #10628, .T. ) ;
#10821=CARTESIAN_POINT ( 'NONE',  ( 2.789999999999999147, 11.04103753892271556, 8.624777288397840636 ) ) ;
#10824=DIRECTION ( 'NONE',  ( 0.000000000000000000, 1.000000000000000000, 1.030528797609984825E-14 ) ) ;
#10826=EDGE_CURVE ( 'NONE', #11452, #7572, #757, .T. ) ;
#10827=VERTEX_POINT ( 'NONE', #14124 ) ;
#10832=VERTEX_POINT ( 'NONE', #1516 ) ;
#10833=CARTESIAN_POINT ( 'NONE',  ( 2.789999999999999147, -9.999777909380009433, 11.07980565117276761 ) ) ;
#10834=CARTESIAN_POINT ( 'NONE',  ( 0.07473581742173487918, -5.299647274067002201, -14.31752701692942153 ) ) ;
#10835=CARTESIAN_POINT ( 'NONE',  ( 0.7795480803411078963, 16.99607982911242132, 4.029281904976690143 ) ) ;
#10840=EDGE_CURVE ( 'NONE', #10809, #1007, #11406, .T. ) ;
#10847=DIRECTION ( 'NONE',  ( -1.000000000000000000, 0.000000000000000000, 0.000000000000000000 ) ) ;
#10849=DIRECTION ( 'NONE',  ( 0.000000000000000000, 0.000000000000000000, 1.000000000000000000 ) ) ;
#10851=AXIS2_PLACEMENT_3D ( 'NONE', #8988, #4310, #2004 ) ;
#10853=DIRECTION ( 'NONE',  ( -1.000000000000000000, -0.000000000000000000, -0.000000000000000000 ) ) ;
#10861=DIRECTION ( 'NONE',  ( -1.000000000000000000, -0.000000000000000000, -0.000000000000000000 ) ) ;
#10869=ADVANCED_FACE ( 'NONE', ( #5297 ), #6430, .T. ) ;
#10876=CARTESIAN_POINT ( 'NONE',  ( 1.749999999999999778, -4.458161950358378256, -17.39253030560846369 ) ) ;
#10893=EDGE_CURVE ( 'NONE', #4933, #6652, #728, .T. ) ;
#10900=CARTESIAN_POINT ( 'NONE',  ( 0.7686372158811266564, -12.71987259277443627, 11.98841295390592876 ) ) ;
#10901=CARTESIAN_POINT ( 'NONE',  ( 0.7686372430964724112, -17.00993931356764222, 4.022333916463534997 ) ) ;
#10905=CARTESIAN_POINT ( 'NONE',  ( 1.039999999999996261, -4.835383649608352208, -17.29145405592693763 ) ) ;
#10906=B_SPLINE_CURVE_WITH_KNOTS ( 'NONE', 3,
 ( #1764, #10987, #519, #2993 ),
 .UNSPECIFIED., .F., .F.,
 ( 4, 4 ),
 ( 1.988537749986050620E-07, 0.0006916721208754055515 ),
 .UNSPECIFIED. ) ;
#10914=EDGE_LOOP ( 'NONE', ( #2738, #8194, #13770, #4579, #1257, #12329, #5633, #7953 ) ) ;
#10941=CYLINDRICAL_SURFACE ( 'NONE', #8305, 8.400000000000000355 ) ;
#10942=ADVANCED_FACE ( 'NONE', ( #13506 ), #10051, .T. ) ;
#10956=CIRCLE ( 'NONE', #6796, 14.01039946648074341 ) ;
#10960=CARTESIAN_POINT ( 'NONE',  ( 2.764680872513208154, 9.232963481057765875, 11.36963888406690870 ) ) ;
#10963=DIRECTION ( 'NONE',  ( -1.000000000000000000, 0.000000000000000000, 0.000000000000000000 ) ) ;
#10970=ADVANCED_FACE ( 'NONE', ( #1677 ), #9693, .T. ) ;
#10979=CARTESIAN_POINT ( 'NONE',  ( 2.021362784118869715, -11.98841295390606554, 12.71987259277430837 ) ) ;
#10983=VECTOR ( 'NONE', #1970, 1000.000000000000000 ) ;
#10985=VERTEX_POINT ( 'NONE', #7596 ) ;
#10987=CARTESIAN_POINT ( 'NONE',  ( 2.782672486186223093, 5.204526028255688885, 13.44898112152240266 ) ) ;
#10995=ORIENTED_EDGE ( 'NONE', *, *, #5658, .F. ) ;
#10996=CARTESIAN_POINT ( 'NONE',  ( 2.789999999999999147, -11.04103753892265694, -8.624777288397918795 ) ) ;
#10997=VECTOR ( 'NONE', #10162, 1000.000000000000000 ) ;
#11010=B_SPLINE_CURVE_WITH_KNOTS ( 'NONE', 3,
 ( #5158, #8591, #1451, #10821 ),
 .UNSPECIFIED., .F., .F.,
 ( 4, 4 ),
 ( 2.451234579287542699E-07, 0.0006917187676826499999 ),
 .UNSPECIFIED. ) ;
#11014=AXIS2_PLACEMENT_3D ( 'NONE', #8105, #4727, #2189 ) ;
#11026=DIRECTION ( 'NONE',  ( -1.000000000000000000, -0.000000000000000000, -0.000000000000000000 ) ) ;
#11028=EDGE_CURVE ( 'NONE', #7572, #5935, #8971, .T. ) ;
#11036=ORIENTED_EDGE ( 'NONE', *, *, #6185, .T. ) ;
#11041=DIRECTION ( 'NONE',  ( 0.000000000000000000, 0.8660254037844433705, -0.4999999999999918954 ) ) ;
#11054=CARTESIAN_POINT ( 'NONE',  ( 1.039999999999999369, 12.55714665599987079, 12.83329210556836308 ) ) ;
#11063=CARTESIAN_POINT ( 'NONE',  ( 0.7795480803411072301, -16.99607982911238935, -4.029281904976810935 ) ) ;
#11068=CARTESIAN_POINT ( 'NONE',  ( 2.337784053193427081, 11.13074453164202993, 12.42068120944084697 ) ) ;
#11072=FILL_AREA_STYLE_COLOUR ( '', #12176 ) ;
#11075=VERTEX_POINT ( 'NONE', #10119 ) ;
#11077=CARTESIAN_POINT ( 'NONE',  ( 2.764680872515351329, -11.36963888406680923, -9.232963481057881339 ) ) ;
#11083=VERTEX_POINT ( 'NONE', #4362 ) ;
#11089=FACE_OUTER_BOUND ( 'NONE', #1795, .T. ) ;
#11093=CARTESIAN_POINT ( 'NONE',  ( 0.000000000000000000, 13.87420763704361448, -1.948757464274226470 ) ) ;
#11105=AXIS2_PLACEMENT_3D ( 'NONE', #3405, #11611, #5791 ) ;
#11106=EDGE_LOOP ( 'NONE', ( #3367, #13695, #319, #6471 ) ) ;
#11107=ORIENTED_EDGE ( 'NONE', *, *, #13622, .T. ) ;
#11120=VERTEX_POINT ( 'NONE', #7963 ) ;
#11125=CARTESIAN_POINT ( 'NONE',  ( 2.789999999999999147, 7.739906618939895289, -10.88091150984218380 ) ) ;
#11134=DIRECTION ( 'NONE',  ( -1.000000000000000000, -0.000000000000000000, -0.000000000000000000 ) ) ;
#11136=AXIS2_PLACEMENT_3D ( 'NONE', #9998, #14700, #10790 ) ;
#11145=CARTESIAN_POINT ( 'NONE',  ( 2.782672435525938681, -11.23174270417322695, -9.044896821682320009 ) ) ;
#11149=AXIS2_PLACEMENT_3D ( 'NONE', #14594, #4066, #588 ) ;
#11155=DIRECTION ( 'NONE',  ( 0.000000000000000000, 0.000000000000000000, 1.000000000000000000 ) ) ;
#11159=DIRECTION ( 'NONE',  ( 0.000000000000000000, 0.000000000000000000, 1.000000000000000000 ) ) ;
#11164=VERTEX_POINT ( 'NONE', #9641 ) ;
#11165=DIRECTION ( 'NONE',  ( 0.000000000000000000, 0.000000000000000000, 1.000000000000000000 ) ) ;
#11170=CARTESIAN_POINT ( 'NONE',  ( -6.210711756101269051E-14, 5.211197193340876943, -13.21862218141511036 ) ) ;
#11171=AXIS2_PLACEMENT_3D ( 'NONE', #1731, #11026, #6188 ) ;
#11178=CARTESIAN_POINT ( 'NONE',  ( 2.789999999999999147, -8.624777288397876163, 11.04103753892268713 ) ) ;
#11183=CIRCLE ( 'NONE', #1128, 14.01039946648074341 ) ;
#11199=B_SPLINE_CURVE_WITH_KNOTS ( 'NONE', 3,
 ( #10807, #2581, #12262, #262, #4977, #13331, #13261, #10876 ),
 .UNSPECIFIED., .F., .F.,
 ( 4, 2, 2, 4 ),
 ( 2.154797737796021283E-07, 0.001895231411415137677, 0.002842739377235819348, 0.003790247343056500368 ),
 .UNSPECIFIED. ) ;
#11201=CARTESIAN_POINT ( 'NONE',  ( 2.771810350101906906, 13.58893811801144658, -5.219853812240780044 ) ) ;
#11209=AXIS2_PLACEMENT_3D ( 'NONE', #11758, #9375, #12980 ) ;
#11213=CARTESIAN_POINT ( 'NONE',  ( 2.789999999999999147, -14.19996452731192527, 4.595504208219980846 ) ) ;
#11223=B_SPLINE_CURVE_WITH_KNOTS ( 'NONE', 3,
 ( #14178, #4582, #14252, #1260 ),
 .UNSPECIFIED., .F., .F.,
 ( 4, 4 ),
 ( 1.988537749986050620E-07, 0.0006916721208754038168 ),
 .UNSPECIFIED. ) ;
#11228=ORIENTED_EDGE ( 'NONE', *, *, #13312, .F. ) ;
#11231=CARTESIAN_POINT ( 'NONE',  ( 0.02531912748464804769, 9.232963481057765875, 11.36963888406690870 ) ) ;
#11235=CARTESIAN_POINT ( 'NONE',  ( 2.789999999999999147, 9.232963481057765875, 11.36963888406690870 ) ) ;
#11236=DIRECTION ( 'NONE',  ( -1.000000000000000000, -0.000000000000000000, -0.000000000000000000 ) ) ;
#11245=AXIS2_PLACEMENT_3D ( 'NONE', #10805, #8408, #5210 ) ;
#11250=EDGE_LOOP ( 'NONE', ( #8524, #430, #13125, #11335 ) ) ;
#11257=CARTESIAN_POINT ( 'NONE',  ( 0.000000000000000000, 7.739906618939895289, -10.88091150984218380 ) ) ;
#11258=AXIS2_PLACEMENT_3D ( 'NONE', #6896, #191, #4602 ) ;
#11271=CIRCLE ( 'NONE', #13733, 17.95481323787947403 ) ;
#11278=CARTESIAN_POINT ( 'NONE',  ( 0.000000000000000000, 7.739906618939707883, 13.40591150984229252 ) ) ;
#11289=ORIENTED_EDGE ( 'NONE', *, *, #14220, .F. ) ;
#11292=DIRECTION ( 'NONE',  ( -1.000000000000000000, 0.000000000000000000, 0.000000000000000000 ) ) ;
#11299=ADVANCED_FACE ( 'NONE', ( #12256 ), #13384, .T. ) ;
#11301=CARTESIAN_POINT ( 'NONE',  ( 2.508169649284527125, 15.84037596932108194, 3.072260951847586963 ) ) ;
#11303=ORIENTED_EDGE ( 'NONE', *, *, #8580, .T. ) ;
#11315=DIRECTION ( 'NONE',  ( -1.000000000000000000, -0.000000000000000000, -0.000000000000000000 ) ) ;
#11331=CARTESIAN_POINT ( 'NONE',  ( 0.02531912748679129854, -9.232963481057844035, 11.36963888406684298 ) ) ;
#11334=DIRECTION ( 'NONE',  ( 0.000000000000000000, 0.000000000000000000, 1.000000000000000000 ) ) ;
#11335=ORIENTED_EDGE ( 'NONE', *, *, #10555, .T. ) ;
#11339=ORIENTED_EDGE ( 'NONE', *, *, #5998, .F. ) ;
#11347=CARTESIAN_POINT ( 'NONE',  ( 2.787323717450090221, 13.26666194250901931, -5.214906618938620397 ) ) ;
#11348=EDGE_LOOP ( 'NONE', ( #14826, #3719, #3640, #6555 ) ) ;
#11353=CARTESIAN_POINT ( 'NONE',  ( 1.039999999999996261, -17.29145405592685592, -4.835383649608655077 ) ) ;
#11354=ADVANCED_FACE ( 'NONE', ( #329 ), #488, .F. ) ;
#11357=CYLINDRICAL_SURFACE ( 'NONE', #142, 8.400000000000000355 ) ;
#11362=FACE_OUTER_BOUND ( 'NONE', #266, .T. ) ;
#11365=CYLINDRICAL_SURFACE ( 'NONE', #14852, 2.524999999999999467 ) ;
#11366=CARTESIAN_POINT ( 'NONE',  ( 1.749999999999999778, 0.000000000000000000, 0.000000000000000000 ) ) ;
#11369=CARTESIAN_POINT ( 'NONE',  ( 2.789999999999999147, -13.87420763704359850, -1.948757464274317508 ) ) ;
#11380=CARTESIAN_POINT ( 'NONE',  ( 0.02531912748679129854, -9.232963481057844035, 11.36963888406684298 ) ) ;
#11389=CYLINDRICAL_SURFACE ( 'NONE', #13386, 17.95481323787947403 ) ;
#11395=ORIENTED_EDGE ( 'NONE', *, *, #3451, .T. ) ;
#11396=VECTOR ( 'NONE', #6383, 1000.000000000000000 ) ;
#11404=EDGE_CURVE ( 'NONE', #13491, #8235, #3566, .T. ) ;
#11405=CARTESIAN_POINT ( 'NONE',  ( 1.039999999999996261, 4.458161950358501713, 17.39253030560843172 ) ) ;
#11406=B_SPLINE_CURVE_WITH_KNOTS ( 'NONE', 3,
 ( #3671, #7135, #200, #11806, #3515, #6133, #115, #8202 ),
 .UNSPECIFIED., .F., .F.,
 ( 4, 2, 2, 4 ),
 ( 4.663089536324781369E-07, 0.001898630414085404096, 0.002847712466651293635, 0.003796794519217182740 ),
 .UNSPECIFIED. ) ;
#11407=VERTEX_POINT ( 'NONE', #10175 ) ;
#11412=CARTESIAN_POINT ( 'NONE',  ( 2.740856711021125047, -13.98777112126107802, 5.263533129984309333 ) ) ;
#11416=CARTESIAN_POINT ( 'NONE',  ( 2.789999999999999147, 12.98979500319701508, -5.249430348645618416 ) ) ;
#11430=FACE_OUTER_BOUND ( 'NONE', #10376, .T. ) ;
#11433=EDGE_LOOP ( 'NONE', ( #11870, #12214, #1251, #5244 ) ) ;
#11438=CARTESIAN_POINT ( 'NONE',  ( 2.789999999999999147, 13.40591150984237245, -7.739906618939567551 ) ) ;
#11439=CARTESIAN_POINT ( 'NONE',  ( 0.02531912748464718033, -9.232963481057685939, -11.36963888406697087 ) ) ;
#11443=CARTESIAN_POINT ( 'NONE',  ( 2.021362756903528179, 17.00993931356761379, 4.022333916463652237 ) ) ;
#11452=VERTEX_POINT ( 'NONE', #14797 ) ;
#11464=CARTESIAN_POINT ( 'NONE',  ( 2.789999999999999147, -12.98979500319690317, -5.249430348645892863 ) ) ;
#11481=LINE ( 'NONE', #15104, #10285 ) ;
#11491=DIRECTION ( 'NONE',  ( 0.000000000000000000, 0.000000000000000000, 1.000000000000000000 ) ) ;
#11494=CARTESIAN_POINT ( 'NONE',  ( 2.700582527824513690, 14.29395843996386262, 5.279841123860917307 ) ) ;
#11495=VECTOR ( 'NONE', #7902, 1000.000000000000000 ) ;
#11498=FACE_BOUND ( 'NONE', #5753, .T. ) ;
#11506=DIRECTION ( 'NONE',  ( 0.000000000000000000, 0.8660254037844433705, -0.4999999999999918954 ) ) ;
#11508=ORIENTED_EDGE ( 'NONE', *, *, #630, .F. ) ;
#11511=CARTESIAN_POINT ( 'NONE',  ( 2.777258977888996672, -13.49735377262296332, -5.214906618939849636 ) ) ;
#11518=CARTESIAN_POINT ( 'NONE',  ( 1.749999999999999778, -17.29145405592685236, -4.835383649608663070 ) ) ;
#11524=ORIENTED_EDGE ( 'NONE', *, *, #5906, .T. ) ;
#11525=ORIENTED_EDGE ( 'NONE', *, *, #13306, .T. ) ;
#11528=AXIS2_PLACEMENT_3D ( 'NONE', #13905, #1224, #1068 ) ;
#11529=CARTESIAN_POINT ( 'NONE',  ( 1.749999999999999778, -12.83329210556841282, 12.55714665599981927 ) ) ;
#11535=CARTESIAN_POINT ( 'NONE',  ( -9.886993524391892676E-15, -14.05347802000167690, -2.096460570596322182 ) ) ;
#11539=CARTESIAN_POINT ( 'NONE',  ( 1.039999999999998037, -4.458161950358621617, 17.39253030560839974 ) ) ;
#11542=EDGE_CURVE ( 'NONE', #6646, #8949, #4560, .T. ) ;
#11550=B_SPLINE_CURVE_WITH_KNOTS ( 'NONE', 3,
 ( #14562, #7257, #1723, #9713, #4025, #2727, #14493, #8699 ),
 .UNSPECIFIED., .F., .F.,
 ( 4, 2, 2, 4 ),
 ( 4.663089536324781899E-07, 0.001898630414085405180, 0.002847712466651292334, 0.003796794519217179704 ),
 .UNSPECIFIED. ) ;
#11554=B_SPLINE_CURVE_WITH_KNOTS ( 'NONE', 3,
 ( #14606, #3075, #4077, #13447 ),
 .UNSPECIFIED., .F., .F.,
 ( 4, 4 ),
 ( 0.005123713096549392838, 0.005814346476695830997 ),
 .UNSPECIFIED. ) ;
#11558=DIRECTION ( 'NONE',  ( -1.000000000000000000, -0.000000000000000000, -0.000000000000000000 ) ) ;
#11561=CYLINDRICAL_SURFACE ( 'NONE', #6792, 2.524999999999999467 ) ;
#11563=ORIENTED_EDGE ( 'NONE', *, *, #14002, .T. ) ;
#11564=DIRECTION ( 'NONE',  ( 0.000000000000000000, 0.000000000000000000, 1.000000000000000000 ) ) ;
#11565=CIRCLE ( 'NONE', #13540, 17.95481323787947403 ) ;
#11567=DIRECTION ( 'NONE',  ( -1.000000000000000000, 0.000000000000000000, 0.000000000000000000 ) ) ;
#11577=VERTEX_POINT ( 'NONE', #14083 ) ;
#11581=EDGE_LOOP ( 'NONE', ( #8395, #1317, #4656, #9147, #10397, #5792 ) ) ;
#11589=VECTOR ( 'NONE', #6620, 1000.000000000000000 ) ;
#11595=LINE ( 'NONE', #12673, #9924 ) ;
#11602=LINE ( 'NONE', #15160, #1402 ) ;
#11604=CARTESIAN_POINT ( 'NONE',  ( 0.09203962824862119141, -9.756102650610156246, -11.73065272960073457 ) ) ;
#11607=ORIENTED_EDGE ( 'NONE', *, *, #3343, .F. ) ;
#11611=DIRECTION ( 'NONE',  ( -1.000000000000000000, -0.000000000000000000, -0.000000000000000000 ) ) ;
#11614=DIRECTION ( 'NONE',  ( 0.000000000000000000, 0.000000000000000000, 1.000000000000000000 ) ) ;
#11620=ORIENTED_EDGE ( 'NONE', *, *, #3602, .F. ) ;
#11626=CIRCLE ( 'NONE', #6732, 2.524999999999999023 ) ;
#11635=AXIS2_PLACEMENT_3D ( 'NONE', #1842, #2770, #14691 ) ;
#11638=CARTESIAN_POINT ( 'NONE',  ( 2.697960317788777207, 5.280991956247118146, 14.31435947614544091 ) ) ;
#11653=EDGE_LOOP ( 'NONE', ( #2763, #9547, #10718, #1449, #13538, #11339, #14782 ) ) ;
#11654=CARTESIAN_POINT ( 'NONE',  ( 0.000000000000000000, -12.98979500319690850, -5.249430348645889310 ) ) ;
#11655=CARTESIAN_POINT ( 'NONE',  ( 1.749999999999999778, -17.39253030560844948, 4.458161950358431547 ) ) ;
#11656=CARTESIAN_POINT ( 'NONE',  ( 0.4522159317772150855, 5.191253194756014544, 15.84984805378633688 ) ) ;
#11660=AXIS2_PLACEMENT_3D ( 'NONE', #13610, #1549, #5107 ) ;
#11663=VERTEX_POINT ( 'NONE', #7246 ) ;
#11669=ORIENTED_EDGE ( 'NONE', *, *, #4717, .T. ) ;
#11672=ORIENTED_EDGE ( 'NONE', *, *, #4802, .F. ) ;
#11676=CARTESIAN_POINT ( 'NONE',  ( 8.000000000000000000, 0.000000000000000000, 0.000000000000000000 ) ) ;
#11678=ADVANCED_FACE ( 'NONE', ( #4951 ), #3778, .T. ) ;
#11680=CARTESIAN_POINT ( 'NONE',  ( 0.04999671152047817368, -2.439987328296867819, -14.75565684666129762 ) ) ;
#11681=EDGE_CURVE ( 'NONE', #4006, #12755, #11183, .T. ) ;
#11700=CARTESIAN_POINT ( 'NONE',  ( 1.749999999999999778, -17.29145405592692342, 4.835383649608411716 ) ) ;
#11704=CARTESIAN_POINT ( 'NONE',  ( 0.000000000000000000, 12.98979500319694225, 5.249430348645796940 ) ) ;
#11719=AXIS2_PLACEMENT_3D ( 'NONE', #5757, #1924, #5615 ) ;
#11723=LINE ( 'NONE', #4745, #2420 ) ;
#11732=DIRECTION ( 'NONE',  ( -1.000000000000000000, -0.000000000000000000, -0.000000000000000000 ) ) ;
#11736=CARTESIAN_POINT ( 'NONE',  ( 1.394999999999999574, -12.83329210556822986, -12.55714665600000757 ) ) ;
#11739=CARTESIAN_POINT ( 'NONE',  ( 0.02531912748606228100, 5.229914364928351489, 13.68080036884350292 ) ) ;
#11747=B_SPLINE_CURVE_WITH_KNOTS ( 'NONE', 3,
 ( #9452, #8530, #2700, #14146, #8302, #2472, #7395, #452 ),
 .UNSPECIFIED., .F., .F.,
 ( 4, 2, 2, 4 ),
 ( 4.663089416196450148E-07, 0.001898630173449458464, 0.002847712105703373645, 0.003796794037957288825 ),
 .UNSPECIFIED. ) ;
#11758=CARTESIAN_POINT ( 'NONE',  ( 2.789999999999999147, 0.000000000000000000, 0.000000000000000000 ) ) ;
#11761=DIRECTION ( 'NONE',  ( 0.000000000000000000, 0.000000000000000000, 1.000000000000000000 ) ) ;
#11769=ADVANCED_FACE ( 'NONE', ( #13468 ), #13305, .T. ) ;
#11772=ORIENTED_EDGE ( 'NONE', *, *, #6764, .T. ) ;
#11774=AXIS2_PLACEMENT_3D ( 'NONE', #14338, #13087, #8641 ) ;
#11775=ORIENTED_EDGE ( 'NONE', *, *, #9872, .T. ) ;
#11776=CARTESIAN_POINT ( 'NONE',  ( -1.092452291144053154E-14, 14.05347802000169288, 2.096460570596223594 ) ) ;
#11780=ORIENTED_EDGE ( 'NONE', *, *, #13497, .T. ) ;
#11785=CARTESIAN_POINT ( 'NONE',  ( 0.5537796877189846700, -12.52687487503410679, -11.41743294611088189 ) ) ;
#11788=CARTESIAN_POINT ( 'NONE',  ( 2.021362740937215019, 5.021526291670316056, 16.74220655292939242 ) ) ;
#11798=EDGE_CURVE ( 'NONE', #11164, #8896, #6780, .T. ) ;
#11799=EDGE_CURVE ( 'NONE', #1932, #3376, #8850, .T. ) ;
#11802=VERTEX_POINT ( 'NONE', #7784 ) ;
#11803=CARTESIAN_POINT ( 'NONE',  ( 0.02531912748464804769, 9.232963481057765875, 11.36963888406690870 ) ) ;
#11805=DIRECTION ( 'NONE',  ( -1.000000000000000000, -0.000000000000000000, 0.000000000000000000 ) ) ;
#11806=CARTESIAN_POINT ( 'NONE',  ( 2.508169719062757874, 10.58084377126639630, -12.18203740414256231 ) ) ;
#11828=CARTESIAN_POINT ( 'NONE',  ( 2.764680872513933796, 5.229914364928542447, -13.68080036884343009 ) ) ;
#11830=CARTESIAN_POINT ( 'NONE',  ( 1.749999999999999778, 12.83329210556831690, 12.55714665599991875 ) ) ;
#11841=DIRECTION ( 'NONE',  ( -1.000000000000000000, 0.000000000000000000, 0.000000000000000000 ) ) ;
#11843=CARTESIAN_POINT ( 'NONE',  ( 0.000000000000000000, -7.739906618939614624, -10.88091150984234545 ) ) ;
#11847=ADVANCED_FACE ( 'NONE', ( #5167 ), #6525, .T. ) ;
#11850=EDGE_LOOP ( 'NONE', ( #14162, #13150, #7673, #15091 ) ) ;
#11857=CARTESIAN_POINT ( 'NONE',  ( 8.000000000000000000, 0.000000000000000000, 0.000000000000000000 ) ) ;
#11867=ORIENTED_EDGE ( 'NONE', *, *, #11798, .T. ) ;
#11870=ORIENTED_EDGE ( 'NONE', *, *, #10454, .T. ) ;
#11878=CARTESIAN_POINT ( 'NONE',  ( -6.133727067292549495E-14, 11.12234047011202875, -8.842064619038410456 ) ) ;
#11880=CARTESIAN_POINT ( 'NONE',  ( 2.010451917295049906, 5.008579424861795637, -16.73367785739752378 ) ) ;
#11883=VERTEX_POINT ( 'NONE', #2836 ) ;
#11884=CARTESIAN_POINT ( 'NONE',  ( 0.000000000000000000, 0.000000000000000000, 0.000000000000000000 ) ) ;
#11887=VECTOR ( 'NONE', #6472, 1000.000000000000000 ) ;
#11895=ORIENTED_EDGE ( 'NONE', *, *, #10373, .F. ) ;
#11896=EDGE_LOOP ( 'NONE', ( #639, #6201, #14614, #6277 ) ) ;
#11902=DIRECTION ( 'NONE',  ( 0.000000000000000000, 0.000000000000000000, 1.000000000000000000 ) ) ;
#11905=EDGE_CURVE ( 'NONE', #14639, #1922, #9759, .T. ) ;
#11906=CARTESIAN_POINT ( 'NONE',  ( 1.039999999999998037, -4.458161950358621617, 17.39253030560839974 ) ) ;
#11910=ORIENTED_EDGE ( 'NONE', *, *, #9458, .T. ) ;
#11920=CARTESIAN_POINT ( 'NONE',  ( 2.021362756903531288, -17.00993931356758537, -4.022333916463769476 ) ) ;
#11921=EDGE_CURVE ( 'NONE', #11083, #4547, #12426, .T. ) ;
#11922=DIRECTION ( 'NONE',  ( 0.000000000000000000, -1.000000000000000000, -3.435095992033282750E-15 ) ) ;
#11932=CARTESIAN_POINT ( 'NONE',  ( -1.014714340245882228E-14, -13.21889893246979142, 5.211150952915317269 ) ) ;
#11933=ORIENTED_EDGE ( 'NONE', *, *, #11921, .T. ) ;
#11941=ADVANCED_FACE ( 'NONE', ( #4069 ), #8600, .F. ) ;
#11944=CARTESIAN_POINT ( 'NONE',  ( 2.715264182578263963, -5.299647274067199376, 14.31752701692935403 ) ) ;
#11945=DIRECTION ( 'NONE',  ( -1.000000000000000000, 0.000000000000000000, 0.000000000000000000 ) ) ;
#11954=CARTESIAN_POINT ( 'NONE',  ( 0.002680699106061737880, 13.26676317347984657, -5.214906618939570748 ) ) ;
#11958=CARTESIAN_POINT ( 'NONE',  ( 0.7795480827049465766, 5.008579424861561158, 16.73367785739759128 ) ) ;
#11961=CARTESIAN_POINT ( 'NONE',  ( 2.597943565934061283, 5.295083827234923213, -14.93837896275544352 ) ) ;
#11969=DIRECTION ( 'NONE',  ( -1.000000000000000000, -0.000000000000000000, 0.000000000000000000 ) ) ;
#11972=CARTESIAN_POINT ( 'NONE',  ( 2.236220346785067647, 16.55730827443872855, -3.624349476775184709 ) ) ;
#11983=CARTESIAN_POINT ( 'NONE',  ( 2.236220312281012035, 11.41743294611075399, 12.52687487503423291 ) ) ;
#12002=EDGE_CURVE ( 'NONE', #11083, #14739, #1626, .T. ) ;
#12007=VERTEX_POINT ( 'NONE', #13748 ) ;
#12018=CARTESIAN_POINT ( 'NONE',  ( 1.039999999999996483, -12.55714665599978375, -12.83329210556844835 ) ) ;
#12019=EDGE_CURVE ( 'NONE', #7858, #2455, #828, .T. ) ;
#12024=ORIENTED_EDGE ( 'NONE', *, *, #12546, .F. ) ;
#12028=EDGE_LOOP ( 'NONE', ( #3171, #11669, #7366, #8944 ) ) ;
#12030=ORIENTED_EDGE ( 'NONE', *, *, #5919, .T. ) ;
#12033=B_SPLINE_CURVE_WITH_KNOTS ( 'NONE', 3,
 ( #12729, #13813, #10204, #2055 ),
 .UNSPECIFIED., .F., .F.,
 ( 4, 4 ),
 ( 0.005123742438166215690, 0.005814376014856852300 ),
 .UNSPECIFIED. ) ;
#12036=CARTESIAN_POINT ( 'NONE',  ( 2.236220367026668931, 5.139875429512081872, -16.15122426806984279 ) ) ;
#12040=ORIENTED_EDGE ( 'NONE', *, *, #7849, .F. ) ;
#12053=CARTESIAN_POINT ( 'NONE',  ( -8.731825252408779477E-15, -11.12243880662607332, -8.842327429719214038 ) ) ;
#12062=B_SPLINE_CURVE_WITH_KNOTS ( 'NONE', 3,
 ( #9259, #2262, #2106, #12778 ),
 .UNSPECIFIED., .F., .F.,
 ( 4, 4 ),
 ( 0.005123695899043904586, 0.005814329666474872711 ),
 .UNSPECIFIED. ) ;
#12075=CARTESIAN_POINT ( 'NONE',  ( 1.394999999999998685, 12.83329210556831690, 12.55714665599991875 ) ) ;
#12083=LINE ( 'NONE', #1138, #4541 ) ;
#12084=AXIS2_PLACEMENT_3D ( 'NONE', #7415, #13072, #2561 ) ;
#12085=B_SPLINE_CURVE_WITH_KNOTS ( 'NONE', 3,
 ( #1825, #3481, #1106, #9334, #12704, #5384, #7018, #2261 ),
 .UNSPECIFIED., .F., .F.,
 ( 4, 2, 2, 4 ),
 ( 4.663089340421306733E-07, 0.001898630032275575984, 0.002847711893946347668, 0.003796793755617119785 ),
 .UNSPECIFIED. ) ;
#12095=ORIENTED_EDGE ( 'NONE', *, *, #10416, .T. ) ;
#12099=DIRECTION ( 'NONE',  ( 0.000000000000000000, 0.000000000000000000, 1.000000000000000000 ) ) ;
#12103=CARTESIAN_POINT ( 'NONE',  ( 2.790000000000011138, 13.21889893246973813, 5.211150952915412304 ) ) ;
#12112=LINE ( 'NONE', #6138, #12988 ) ;
#12118=VERTEX_POINT ( 'NONE', #8663 ) ;
#12121=CARTESIAN_POINT ( 'NONE',  ( 2.715264205769559958, 15.04916547791930270, -2.569134216958818495 ) ) ;
#12124=ORIENTED_EDGE ( 'NONE', *, *, #8427, .T. ) ;
#12125=ORIENTED_EDGE ( 'NONE', *, *, #13612, .T. ) ;
#12132=AXIS2_PLACEMENT_3D ( 'NONE', #2642, #10853, #312 ) ;
#12133=AXIS2_PLACEMENT_3D ( 'NONE', #12956, #11732, #8273 ) ;
#12135=EDGE_CURVE ( 'NONE', #1922, #12657, #4191, .T. ) ;
#12137=CARTESIAN_POINT ( 'NONE',  ( 2.790000000000000924, 0.000000000000000000, 0.000000000000000000 ) ) ;
#12139=AXIS2_PLACEMENT_3D ( 'NONE', #2905, #3907, #5381 ) ;
#12141=VERTEX_POINT ( 'NONE', #7386 ) ;
#12143=CARTESIAN_POINT ( 'NONE',  ( 2.789999999999999147, -11.04103753892265694, -8.624777288397918795 ) ) ;
#12144=EDGE_CURVE ( 'NONE', #6030, #13716, #13345, .T. ) ;
#12145=CARTESIAN_POINT ( 'NONE',  ( 2.789999999999999147, -13.87420763704359850, -1.948757464274317508 ) ) ;
#12146=ORIENTED_EDGE ( 'NONE', *, *, #10787, .F. ) ;
#12162=DIRECTION ( 'NONE',  ( 1.000000000000000000, -0.000000000000000000, 0.000000000000000000 ) ) ;
#12164=ORIENTED_EDGE ( 'NONE', *, *, #14027, .F. ) ;
#12172=AXIS2_PLACEMENT_3D ( 'NONE', #13816, #4454, #9134 ) ;
#12174=DIRECTION ( 'NONE',  ( -1.000000000000000000, 0.000000000000000000, 0.000000000000000000 ) ) ;
#12176=COLOUR_RGB ( '',1.000000000000000000, 0.9490196078431372140, 0.9098039215686274384 ) ;
#12177=AXIS2_PLACEMENT_3D ( 'NONE', #13729, #3042, #11334 ) ;
#12185=EDGE_CURVE ( 'NONE', #7731, #1772, #13152, .T. ) ;
#12189=DIRECTION ( 'NONE',  ( -1.000000000000000000, 0.000000000000000000, 0.000000000000000000 ) ) ;
#12196=CARTESIAN_POINT ( 'NONE',  ( -10.00000000000000000, 0.000000000000000000, 0.000000000000000000 ) ) ;
#12203=CARTESIAN_POINT ( 'NONE',  ( 0.007327513813774889397, -5.204526028255783920, 13.44898112152236891 ) ) ;
#12204=EDGE_CURVE ( 'NONE', #5435, #12653, #5809, .T. ) ;
#12209=CARTESIAN_POINT ( 'NONE',  ( 2.010451919658913678, 16.99607982911238224, -4.029281904976652839 ) ) ;
#12214=ORIENTED_EDGE ( 'NONE', *, *, #7511, .T. ) ;
#12222=CARTESIAN_POINT ( 'NONE',  ( 2.715264245299034762, 9.749517823374011627, 11.74839219818091607 ) ) ;
#12228=ORIENTED_EDGE ( 'NONE', *, *, #15214, .F. ) ;
#12230=CARTESIAN_POINT ( 'NONE',  ( 2.764680872515352661, -14.46287784598615644, -2.311161484776706576 ) ) ;
#12235=B_SPLINE_CURVE_WITH_KNOTS ( 'NONE', 3,
 ( #2729, #11932, #6028, #6971 ),
 .UNSPECIFIED., .F., .F.,
 ( 4, 4 ),
 ( 0.005123742438166228701, 0.005814376014856857504 ),
 .UNSPECIFIED. ) ;
#12242=AXIS2_PLACEMENT_3D ( 'NONE', #5213, #14269, #7507 ) ;
#12244=AXIS2_PLACEMENT_3D ( 'NONE', #6036, #184, #4096 ) ;
#12245=DIRECTION ( 'NONE',  ( 0.000000000000000000, 0.000000000000000000, -1.000000000000000000 ) ) ;
#12247=FACE_BOUND ( 'NONE', #176, .T. ) ;
#12250=CARTESIAN_POINT ( 'NONE',  ( 2.764680872515352217, 2.311161484776756758, -14.46287784598614756 ) ) ;
#12256=FACE_OUTER_BOUND ( 'NONE', #12623, .T. ) ;
#12257=AXIS2_PLACEMENT_3D ( 'NONE', #13138, #222, #8154 ) ;
#12260=CARTESIAN_POINT ( 'NONE',  ( 2.789999999999999147, -2.311161484776655950, 14.46287784598616355 ) ) ;
#12262=CARTESIAN_POINT ( 'NONE',  ( 2.597943646031690257, -2.883512197588903092, -15.58455734132169468 ) ) ;
#12267=ADVANCED_FACE ( 'NONE', ( #10207 ), #11357, .T. ) ;
#12272=CARTESIAN_POINT ( 'NONE',  ( 2.789999999999999147, 14.59528211760002137, -3.120158876139080828 ) ) ;
#12278=EDGE_CURVE ( 'NONE', #3477, #2567, #4375, .T. ) ;
#12285=DIRECTION ( 'NONE',  ( -1.000000000000000000, -0.000000000000000000, -0.000000000000000000 ) ) ;
#12295=EDGE_CURVE ( 'NONE', #4006, #4933, #3588, .T. ) ;
#12296=CARTESIAN_POINT ( 'NONE',  ( 2.597943782557557757, 10.28947301956282345, 12.05486625177575455 ) ) ;
#12298=ORIENTED_EDGE ( 'NONE', *, *, #4930, .T. ) ;
#12308=DIRECTION ( 'NONE',  ( -1.000000000000000000, -0.000000000000000000, -0.000000000000000000 ) ) ;
#12312=CARTESIAN_POINT ( 'NONE',  ( 2.789999999999999147, -1.948757464274075479, -13.87420763704363225 ) ) ;
#12313=AXIS2_PLACEMENT_3D ( 'NONE', #4976, #3729, #7274 ) ;
#12317=CARTESIAN_POINT ( 'NONE',  ( 0.01274102211100516108, 13.49735377262310720, -5.214906618939568084 ) ) ;
#12322=CARTESIAN_POINT ( 'NONE',  ( 1.749999999999999778, -4.458161950358622505, 17.39253030560840330 ) ) ;
#12324=CIRCLE ( 'NONE', #9623, 2.524999999999999467 ) ;
#12329=ORIENTED_EDGE ( 'NONE', *, *, #10787, .T. ) ;
#12333=B_SPLINE_CURVE_WITH_KNOTS ( 'NONE', 3,
 ( #11405, #4353, #3128, #5440, #4503, #9184, #12635, #882 ),
 .UNSPECIFIED., .F., .F.,
 ( 4, 2, 2, 4 ),
 ( 4.663089416215518448E-07, 0.001898630173449453477, 0.002847712105703369741, 0.003796794037957286223 ),
 .UNSPECIFIED. ) ;
#12336=ORIENTED_EDGE ( 'NONE', *, *, #5155, .T. ) ;
#12340=EDGE_CURVE ( 'NONE', #13265, #11577, #7907, .T. ) ;
#12344=CARTESIAN_POINT ( 'NONE',  ( -5.209999999999999964, 0.000000000000000000, 0.000000000000000000 ) ) ;
#12349=CARTESIAN_POINT ( 'NONE',  ( 2.021362756903528624, 4.022333916463829873, -17.00993931356757116 ) ) ;
#12351=EDGE_CURVE ( 'NONE', #6770, #1400, #6295, .T. ) ;
#12352=FACE_OUTER_BOUND ( 'NONE', #9350, .T. ) ;
#12354=DIRECTION ( 'NONE',  ( -1.000000000000000000, -0.000000000000000000, 0.000000000000000000 ) ) ;
#12361=EDGE_CURVE ( 'NONE', #6679, #1826, #6787, .T. ) ;
#12378=CARTESIAN_POINT ( 'NONE',  ( 2.764680872513682885, -14.46287784598619020, 2.311161484776505404 ) ) ;
#12389=CARTESIAN_POINT ( 'NONE',  ( 0.02531912748464631296, -13.68080036884344963, -5.229914364928496262 ) ) ;
#12398=CARTESIAN_POINT ( 'NONE',  ( 0.02531912748605881155, 13.68080036884355621, -5.229914364928207604 ) ) ;
#12400=VERTEX_POINT ( 'NONE', #404 ) ;
#12403=AXIS2_PLACEMENT_3D ( 'NONE', #6011, #8544, #9698 ) ;
#12404=CIRCLE ( 'NONE', #7748, 2.524999999999999023 ) ;
#12408=CARTESIAN_POINT ( 'NONE',  ( 2.789999999999999147, -11.36963888406694068, 9.232963481057725019 ) ) ;
#12418=LINE ( 'NONE', #8880, #9262 ) ;
#12426=B_SPLINE_CURVE_WITH_KNOTS ( 'NONE', 3,
 ( #14529, #10901, #515, #3837, #3992, #14458, #8664, #14600 ),
 .UNSPECIFIED., .F., .F.,
 ( 4, 2, 2, 4 ),
 ( 4.663089412835749521E-07, 0.001898630173449111953, 0.002847712105703030603, 0.003796794037956948819 ),
 .UNSPECIFIED. ) ;
#12434=EDGE_CURVE ( 'NONE', #8724, #10827, #12235, .T. ) ;
#12438=EDGE_CURVE ( 'NONE', #3623, #9529, #4084, .T. ) ;
#12442=CIRCLE ( 'NONE', #11209, 14.01039946648073986 ) ;
#12444=ORIENTED_EDGE ( 'NONE', *, *, #1857, .F. ) ;
#12452=CARTESIAN_POINT ( 'NONE',  ( 1.394999999999999574, -4.835383649608592016, 17.29145405592687368 ) ) ;
#12464=DIRECTION ( 'NONE',  ( 1.000000000000000000, 0.000000000000000000, -0.000000000000000000 ) ) ;
#12470=DIRECTION ( 'NONE',  ( -1.000000000000000000, 0.000000000000000000, 0.000000000000000000 ) ) ;
#12473=CARTESIAN_POINT ( 'NONE',  ( 0.02531912748464804769, 9.232963481057765875, 11.36963888406690870 ) ) ;
#12483=DIRECTION ( 'NONE',  ( 0.000000000000000000, 0.000000000000000000, 1.000000000000000000 ) ) ;
#12484=ORIENTED_EDGE ( 'NONE', *, *, #7425, .F. ) ;
#12495=AXIS2_PLACEMENT_3D ( 'NONE', #8045, #1203, #10577 ) ;
#12499=VERTEX_POINT ( 'NONE', #13076 ) ;
#12502=ORIENTED_EDGE ( 'NONE', *, *, #630, .T. ) ;
#12504=ORIENTED_EDGE ( 'NONE', *, *, #13238, .T. ) ;
#12513=CARTESIAN_POINT ( 'NONE',  ( 2.582362678678089551, 2.899259574942964157, -15.57879356040259822 ) ) ;
#12522=CARTESIAN_POINT ( 'NONE',  ( 0.000000000000000000, 0.000000000000000000, 0.000000000000000000 ) ) ;
#12523=FACE_OUTER_BOUND ( 'NONE', #1713, .T. ) ;
#12528=DIRECTION ( 'NONE',  ( 0.000000000000000000, 0.4999999999999891198, 0.8660254037844450359 ) ) ;
#12534=ORIENTED_EDGE ( 'NONE', *, *, #9872, .F. ) ;
#12540=EDGE_CURVE ( 'NONE', #6652, #7725, #6550, .T. ) ;
#12541=ORIENTED_EDGE ( 'NONE', *, *, #5772, .T. ) ;
#12545=CARTESIAN_POINT ( 'NONE',  ( 2.789999999999999147, -12.98979500319690317, -5.249430348645892863 ) ) ;
#12546=EDGE_CURVE ( 'NONE', #9595, #8589, #13409, .T. ) ;
#12557=ORIENTED_EDGE ( 'NONE', *, *, #5267, .F. ) ;
#12560=DIRECTION ( 'NONE',  ( 0.000000000000000000, 0.000000000000000000, 1.000000000000000000 ) ) ;
#12562=ORIENTED_EDGE ( 'NONE', *, *, #3451, .F. ) ;
#12563=B_SPLINE_CURVE_WITH_KNOTS ( 'NONE', 3,
 ( #12721, #9278, #12790, #2277 ),
 .UNSPECIFIED., .F., .F.,
 ( 4, 4 ),
 ( 2.159563976993877881E-07, 0.0006916893629248557470 ),
 .UNSPECIFIED. ) ;
#12571=EDGE_CURVE ( 'NONE', #5551, #8235, #5286, .T. ) ;
#12576=CARTESIAN_POINT ( 'NONE',  ( 2.790000000000061320, 13.12794558796753819, -5.226347720069123071 ) ) ;
#12579=DIRECTION ( 'NONE',  ( 0.000000000000000000, 0.000000000000000000, 1.000000000000000000 ) ) ;
#12582=VERTEX_POINT ( 'NONE', #7642 ) ;
#12583=CARTESIAN_POINT ( 'NONE',  ( 2.789999999999999147, -14.46287784598615644, -2.311161484776706576 ) ) ;
#12588=CARTESIAN_POINT ( 'NONE',  ( 2.782672486186224425, -5.204526028255594738, -13.44898112152243819 ) ) ;
#12593=DIRECTION ( 'NONE',  ( 1.000000000000000000, 0.000000000000000000, 0.000000000000000000 ) ) ;
#12594=CARTESIAN_POINT ( 'NONE',  ( -6.099252894168396215E-14, -8.842064619038449536, -11.12234047011199500 ) ) ;
#12597=DIRECTION ( 'NONE',  ( -1.000000000000000000, -0.000000000000000000, -0.000000000000000000 ) ) ;
#12604=CARTESIAN_POINT ( 'NONE',  ( -9.970929402304026638E-15, -5.211150952915271084, -13.21889893246980918 ) ) ;
#12606=CARTESIAN_POINT ( 'NONE',  ( 2.246812850058910183, -5.154374911958798933, -16.16568790143447032 ) ) ;
#12608=CARTESIAN_POINT ( 'NONE',  ( 0.000000000000000000, -8.624777288397881492, 11.04103753892268891 ) ) ;
#12610=AXIS2_PLACEMENT_3D ( 'NONE', #8137, #2525, #205 ) ;
#12613=DIRECTION ( 'NONE',  ( 0.000000000000000000, 0.000000000000000000, 1.000000000000000000 ) ) ;
#12615=EDGE_CURVE ( 'NONE', #14375, #3154, #8014, .T. ) ;
#12623=EDGE_LOOP ( 'NONE', ( #13064, #4497, #13298, #8217, #3510, #4456, #6181 ) ) ;
#12627=VERTEX_POINT ( 'NONE', #3026 ) ;
#12635=CARTESIAN_POINT ( 'NONE',  ( 0.04999671152047786143, 2.439987328296971736, 14.75565684666128163 ) ) ;
#12637=ORIENTED_EDGE ( 'NONE', *, *, #4222, .F. ) ;
#12642=EDGE_CURVE ( 'NONE', #10760, #5551, #299, .T. ) ;
#12653=VERTEX_POINT ( 'NONE', #6565 ) ;
#12654=DIRECTION ( 'NONE',  ( 1.000000000000000000, 0.000000000000000000, 0.000000000000000000 ) ) ;
#12656=ORIENTED_EDGE ( 'NONE', *, *, #11905, .T. ) ;
#12657=VERTEX_POINT ( 'NONE', #5426 ) ;
#12660=CARTESIAN_POINT ( 'NONE',  ( -10.00000000000000000, 0.000000000000000000, 0.000000000000000000 ) ) ;
#12665=CARTESIAN_POINT ( 'NONE',  ( 2.789999999999999147, -12.98979500319697955, 5.249430348645709010 ) ) ;
#12666=CYLINDRICAL_SURFACE ( 'NONE', #10851, 8.400000000000000355 ) ;
#12673=CARTESIAN_POINT ( 'NONE',  ( 2.789999999999999147, 2.311161484776756758, -14.46287784598614756 ) ) ;
#12674=EDGE_CURVE ( 'NONE', #13716, #4803, #8500, .T. ) ;
#12681=DIRECTION ( 'NONE',  ( -1.000000000000000000, -0.000000000000000000, -0.000000000000000000 ) ) ;
#12684=CARTESIAN_POINT ( 'NONE',  ( 2.582362639458679610, -5.278564329440899705, -14.94126095370966567 ) ) ;
#12686=CARTESIAN_POINT ( 'NONE',  ( 0.007349557670559579703, -9.045126717605857181, 11.23191127083860508 ) ) ;
#12687=VECTOR ( 'NONE', #14045, 1000.000000000000000 ) ;
#12698=CIRCLE ( 'NONE', #7319, 2.524999999999998579 ) ;
#12704=CARTESIAN_POINT ( 'NONE',  ( 2.582362639458678277, 14.94126095370968166, -5.278564329440845526 ) ) ;
#12713=CARTESIAN_POINT ( 'NONE',  ( 0.4522159373304727170, 3.429166897524654534, -16.32199768300075249 ) ) ;
#12720=AXIS2_PLACEMENT_3D ( 'NONE', #10202, #13741, #12579 ) ;
#12721=CARTESIAN_POINT ( 'NONE',  ( 0.02531912748256377743, 14.46287784598617421, -2.311161484776606212 ) ) ;
#12722=CARTESIAN_POINT ( 'NONE',  ( 1.749999999999999778, 4.458161950358502601, 17.39253030560843172 ) ) ;
#12723=ADVANCED_FACE ( 'NONE', ( #7873 ), #11389, .T. ) ;
#12727=B_SPLINE_CURVE_WITH_KNOTS ( 'NONE', 3,
 ( #152, #8458, #10700, #6012, #13234, #4873, #5108, #1398 ),
 .UNSPECIFIED., .F., .F.,
 ( 4, 2, 2, 4 ),
 ( 4.663089342034313692E-07, 0.001898630032275744253, 0.002847711893946512033, 0.003796793755617279813 ),
 .UNSPECIFIED. ) ;
#12729=CARTESIAN_POINT ( 'NONE',  ( 2.789999999999999147, -5.249430348645846678, 12.98979500319692448 ) ) ;
#12732=CIRCLE ( 'NONE', #10536, 2.524999999999999467 ) ;
#12735=ORIENTED_EDGE ( 'NONE', *, *, #12642, .T. ) ;
#12742=CARTESIAN_POINT ( 'NONE',  ( 0.02531912748464674665, 5.229914364928542447, -13.68080036884343009 ) ) ;
#12748=ORIENTED_EDGE ( 'NONE', *, *, #9245, .F. ) ;
#12749=B_SPLINE_CURVE_WITH_KNOTS ( 'NONE', 3,
 ( #2596, #9888, #11961, #14587, #12036, #11880, #504, #1448 ),
 .UNSPECIFIED., .F., .F.,
 ( 4, 2, 2, 4 ),
 ( 1.984117563342667082E-07, 0.001895214258086359458, 0.002842722181251369599, 0.003790230104416379524 ),
 .UNSPECIFIED. ) ;
#12755=VERTEX_POINT ( 'NONE', #9021 ) ;
#12756=ORIENTED_EDGE ( 'NONE', *, *, #2032, .F. ) ;
#12759=CARTESIAN_POINT ( 'NONE',  ( 8.000000000000000000, 0.000000000000000000, 0.000000000000000000 ) ) ;
#12762=EDGE_CURVE ( 'NONE', #6646, #12118, #8229, .T. ) ;
#12774=VERTEX_POINT ( 'NONE', #8162 ) ;
#12778=CARTESIAN_POINT ( 'NONE',  ( 2.764680872513205934, -11.36963888406694068, 9.232963481057725019 ) ) ;
#12784=ORIENTED_EDGE ( 'NONE', *, *, #6937, .F. ) ;
#12785=ORIENTED_EDGE ( 'NONE', *, *, #4425, .T. ) ;
#12790=CARTESIAN_POINT ( 'NONE',  ( -6.138153946363927094E-14, 14.05326139264726315, -2.096282088614805250 ) ) ;
#12791=ADVANCED_FACE ( 'NONE', ( #14953 ), #7938, .T. ) ;
#12793=ORIENTED_EDGE ( 'NONE', *, *, #15179, .T. ) ;
#12797=CARTESIAN_POINT ( 'NONE',  ( 2.789999999999999147, 3.120158876139031534, 14.59528211760003558 ) ) ;
#12803=CARTESIAN_POINT ( 'NONE',  ( 0.1438988480186108865, -14.59528211759996630, 5.279841123860814278 ) ) ;
#12804=ORIENTED_EDGE ( 'NONE', *, *, #4968, .F. ) ;
#12805=LINE ( 'NONE', #11736, #13177 ) ;
#12822=ORIENTED_EDGE ( 'NONE', *, *, #13987, .F. ) ;
#12837=DIRECTION ( 'NONE',  ( -1.000000000000000000, 0.000000000000000000, 0.000000000000000000 ) ) ;
#12845=EDGE_CURVE ( 'NONE', #484, #12141, #12884, .T. ) ;
#12848=AXIS2_PLACEMENT_3D ( 'NONE', #2645, #10789, #165 ) ;
#12850=ORIENTED_EDGE ( 'NONE', *, *, #2847, .F. ) ;
#12852=EDGE_CURVE ( 'NONE', #8452, #1420, #9220, .T. ) ;
#12869=CARTESIAN_POINT ( 'NONE',  ( 0.007349505829628562997, 5.204557061642287152, 13.44926448535267838 ) ) ;
#12871=DIRECTION ( 'NONE',  ( -1.000000000000000000, 0.000000000000000000, 0.000000000000000000 ) ) ;
#12878=CARTESIAN_POINT ( 'NONE',  ( 2.236220312281013811, 12.52687487503435193, -11.41743294611062254 ) ) ;
#12883=AXIS2_PLACEMENT_3D ( 'NONE', #13786, #7942, #13635 ) ;
#12884=CIRCLE ( 'NONE', #12403, 2.524999999999999467 ) ;
#12885=DIRECTION ( 'NONE',  ( 0.000000000000000000, 0.000000000000000000, 1.000000000000000000 ) ) ;
#12886=DIRECTION ( 'NONE',  ( -1.000000000000000000, -0.000000000000000000, -0.000000000000000000 ) ) ;
#12891=ORIENTED_EDGE ( 'NONE', *, *, #113, .F. ) ;
#12894=ORIENTED_EDGE ( 'NONE', *, *, #8230, .F. ) ;
#12906=B_SPLINE_CURVE_WITH_KNOTS ( 'NONE', 3,
 ( #10212, #11511, #14831, #7841 ),
 .UNSPECIFIED., .F., .F.,
 ( 4, 4 ),
 ( 0.005540500595652342840, 0.005814376014856851432 ),
 .UNSPECIFIED. ) ;
#12908=AXIS2_PLACEMENT_3D ( 'NONE', #2399, #10619, #4865 ) ;
#12909=EDGE_CURVE ( 'NONE', #8554, #12141, #119, .T. ) ;
#12912=CARTESIAN_POINT ( 'NONE',  ( 2.789999999999999147, 2.311161484776556030, 14.46287784598618309 ) ) ;
#12932=VECTOR ( 'NONE', #13721, 1000.000000000000000 ) ;
#12938=EDGE_CURVE ( 'NONE', #1316, #3142, #10559, .T. ) ;
#12939=VECTOR ( 'NONE', #14099, 1000.000000000000000 ) ;
#12940=CYLINDRICAL_SURFACE ( 'NONE', #8044, 8.400000000000000355 ) ;
#12946=CARTESIAN_POINT ( 'NONE',  ( 2.236220346785028568, 3.624349476775199808, 16.55730827443882802 ) ) ;
#12956=CARTESIAN_POINT ( 'NONE',  ( 0.000000000000000000, 7.739906618939895289, -13.40591150984218416 ) ) ;
#12959=CARTESIAN_POINT ( 'NONE',  ( 0.2818302809372421058, 10.58084377126623288, 12.18203740414270619 ) ) ;
#12963=CYLINDRICAL_SURFACE ( 'NONE', #14350, 8.400000000000000355 ) ;
#12973=B_SPLINE_CURVE_WITH_KNOTS ( 'NONE', 3,
 ( #11739, #199, #6056, #11656, #114, #11958, #5914, #9513 ),
 .UNSPECIFIED., .F., .F.,
 ( 4, 2, 2, 4 ),
 ( 1.984117563342565173E-07, 0.001895214258086353387, 0.002842722181251365696, 0.003790230104416377789 ),
 .UNSPECIFIED. ) ;
#12980=DIRECTION ( 'NONE',  ( 0.000000000000000000, 0.000000000000000000, 1.000000000000000000 ) ) ;
#12982=CARTESIAN_POINT ( 'NONE',  ( 2.789999999999999147, 1.621424371464993087E-13, -15.47981323787947794 ) ) ;
#12984=AXIS2_PLACEMENT_3D ( 'NONE', #14919, #3080, #9222 ) ;
#12985=CARTESIAN_POINT ( 'NONE',  ( 0.4522159373304753816, -3.429166897524540403, 16.32199768300078802 ) ) ;
#12988=VECTOR ( 'NONE', #6212, 1000.000000000000000 ) ;
#12991=CARTESIAN_POINT ( 'NONE',  ( 1.039999999999998259, -12.83329210556822986, -12.55714665600000757 ) ) ;
#12992=ORIENTED_EDGE ( 'NONE', *, *, #2424, .T. ) ;
#12998=ADVANCED_FACE ( 'NONE', ( #14626 ), #7402, .T. ) ;
#13000=CARTESIAN_POINT ( 'NONE',  ( 1.749999999999999778, -12.55714665599996138, 12.83329210556827249 ) ) ;
#13004=DIRECTION ( 'NONE',  ( 0.000000000000000000, 0.000000000000000000, 1.000000000000000000 ) ) ;
#13026=EDGE_CURVE ( 'NONE', #3477, #1632, #7817, .T. ) ;
#13031=CARTESIAN_POINT ( 'NONE',  ( 1.749999999999999778, -12.83329210556841282, 12.55714665599981927 ) ) ;
#13036=ORIENTED_EDGE ( 'NONE', *, *, #14557, .T. ) ;
#13043=ORIENTED_EDGE ( 'NONE', *, *, #4118, .T. ) ;
#13045=VERTEX_POINT ( 'NONE', #1710 ) ;
#13050=CARTESIAN_POINT ( 'NONE',  ( 0.1920563539683084187, 15.58455734132166981, 2.883512197589065185 ) ) ;
#13051=CARTESIAN_POINT ( 'NONE',  ( 2.236220312281013811, -11.41743294611066339, -12.52687487503431463 ) ) ;
#13060=EDGE_CURVE ( 'NONE', #6955, #5808, #8540, .T. ) ;
#13064=ORIENTED_EDGE ( 'NONE', *, *, #8427, .F. ) ;
#13072=DIRECTION ( 'NONE',  ( -1.000000000000000000, -0.000000000000000000, 0.000000000000000000 ) ) ;
#13076=CARTESIAN_POINT ( 'NONE',  ( 2.781248467066446572, 13.40591150985955871, -5.214906618939568972 ) ) ;
#13078=ORIENTED_EDGE ( 'NONE', *, *, #12852, .T. ) ;
#13083=B_SPLINE_CURVE_WITH_KNOTS ( 'NONE', 3,
 ( #5507, #4348, #13726, #9035 ),
 .UNSPECIFIED., .F., .F.,
 ( 4, 4 ),
 ( 1.988537749986029444E-07, 0.0002742066915202718549 ),
 .UNSPECIFIED. ) ;
#13087=DIRECTION ( 'NONE',  ( -1.000000000000000000, -0.000000000000000000, -0.000000000000000000 ) ) ;
#13089=VERTEX_POINT ( 'NONE', #468 ) ;
#13109=DIRECTION ( 'NONE',  ( 0.000000000000000000, 0.000000000000000000, 1.000000000000000000 ) ) ;
#13116=EDGE_CURVE ( 'NONE', #14810, #11407, #9093, .T. ) ;
#13119=CARTESIAN_POINT ( 'NONE',  ( 1.039999999999996927, 12.55714665600005375, -12.83329210556818545 ) ) ;
#13123=B_SPLINE_CURVE_WITH_KNOTS ( 'NONE', 3,
 ( #14697, #13294, #4166, #2774 ),
 .UNSPECIFIED., .F., .F.,
 ( 4, 4 ),
 ( 2.451234579287565992E-07, 0.0006917187676826499999 ),
 .UNSPECIFIED. ) ;
#13125=ORIENTED_EDGE ( 'NONE', *, *, #9224, .T. ) ;
#13132=CARTESIAN_POINT ( 'NONE',  ( 2.789999999999999147, 5.249430348645936384, -12.98979500319688718 ) ) ;
#13134=EDGE_CURVE ( 'NONE', #5814, #14639, #1379, .T. ) ;
#13138=CARTESIAN_POINT ( 'NONE',  ( -10.00000000000000000, 0.000000000000000000, 0.000000000000000000 ) ) ;
#13139=EDGE_CURVE ( 'NONE', #3376, #7725, #15154, .T. ) ;
#13148=AXIS2_PLACEMENT_3D ( 'NONE', #6459, #11134, #1545 ) ;
#13150=ORIENTED_EDGE ( 'NONE', *, *, #13987, .T. ) ;
#13151=AXIS2_PLACEMENT_3D ( 'NONE', #10062, #12654, #11506 ) ;
#13152=B_SPLINE_CURVE_WITH_KNOTS ( 'NONE', 3,
 ( #9672, #10979, #7609, #444, #3991, #14372, #7533, #5232 ),
 .UNSPECIFIED., .F., .F.,
 ( 4, 2, 2, 4 ),
 ( 4.663089536348421000E-07, 0.001898630414085407565, 0.002847712466651294936, 0.003796794519217182307 ),
 .UNSPECIFIED. ) ;
#13157=DIRECTION ( 'NONE',  ( 1.000000000000000000, 0.000000000000000000, 0.000000000000000000 ) ) ;
#13160=ORIENTED_EDGE ( 'NONE', *, *, #6307, .T. ) ;
#13168=CARTESIAN_POINT ( 'NONE',  ( 0.7795480763126745316, 12.70439593876660567, 11.98750039041498461 ) ) ;
#13175=FACE_OUTER_BOUND ( 'NONE', #14724, .T. ) ;
#13177=VECTOR ( 'NONE', #5839, 1000.000000000000000 ) ;
#13187=EDGE_LOOP ( 'NONE', ( #342, #8103, #1077, #12562, #14527, #6401 ) ) ;
#13193=CIRCLE ( 'NONE', #1662, 14.01039946648074341 ) ;
#13195=DIRECTION ( 'NONE',  ( 0.000000000000000000, 0.000000000000000000, 1.000000000000000000 ) ) ;
#13198=DIRECTION ( 'NONE',  ( -1.000000000000000000, -0.000000000000000000, 0.000000000000000000 ) ) ;
#13212=CARTESIAN_POINT ( 'NONE',  ( 0.02531912748464674665, -11.36963888406694068, 9.232963481057725019 ) ) ;
#13214=VERTEX_POINT ( 'NONE', #9085 ) ;
#13221=EDGE_CURVE ( 'NONE', #1932, #1234, #4106, .T. ) ;
#13222=CARTESIAN_POINT ( 'NONE',  ( 1.749999999999999778, 17.29145405592688789, 4.835383649608534284 ) ) ;
#13223=CARTESIAN_POINT ( 'NONE',  ( 1.885839528871394943, -12.27244837507604025, -12.77651625388912038 ) ) ;
#13227=ORIENTED_EDGE ( 'NONE', *, *, #7879, .F. ) ;
#13234=CARTESIAN_POINT ( 'NONE',  ( 0.2076373605413182333, -14.94126095370957863, -5.278564329441158165 ) ) ;
#13238=EDGE_CURVE ( 'NONE', #12774, #3044, #11602, .T. ) ;
#13240=CYLINDRICAL_SURFACE ( 'NONE', #5989, 2.524999999999999023 ) ;
#13245=CARTESIAN_POINT ( 'NONE',  ( 0.000000000000000000, 1.621424371464993087E-13, -15.47981323787947794 ) ) ;
#13251=VERTEX_POINT ( 'NONE', #9448 ) ;
#13261=CARTESIAN_POINT ( 'NONE',  ( 1.885839517048285119, -4.239993951493086222, -17.20101185194004856 ) ) ;
#13265=VERTEX_POINT ( 'NONE', #2614 ) ;
#13271=CARTESIAN_POINT ( 'NONE',  ( 2.136152509568735258, 16.44008199387299740, 5.087730618022634488 ) ) ;
#13272=ORIENTED_EDGE ( 'NONE', *, *, #790, .F. ) ;
#13275=ORIENTED_EDGE ( 'NONE', *, *, #5919, .F. ) ;
#13277=CARTESIAN_POINT ( 'NONE',  ( 2.789999999999999147, 1.621424371464993087E-13, -15.47981323787947794 ) ) ;
#13279=ADVANCED_FACE ( 'NONE', ( #5993 ), #2386, .T. ) ;
#13284=ORIENTED_EDGE ( 'NONE', *, *, #14622, .F. ) ;
#13286=ORIENTED_EDGE ( 'NONE', *, *, #1986, .F. ) ;
#13287=CARTESIAN_POINT ( 'NONE',  ( -5.209999999999999964, 0.000000000000000000, 0.000000000000000000 ) ) ;
#13289=CARTESIAN_POINT ( 'NONE',  ( 0.000000000000000000, -13.40591150984231916, 7.739906618939660810 ) ) ;
#13294=CARTESIAN_POINT ( 'NONE',  ( 0.007327564474061405535, -11.23174270417335663, 9.044896821682165466 ) ) ;
#13298=ORIENTED_EDGE ( 'NONE', *, *, #9287, .F. ) ;
#13305=CYLINDRICAL_SURFACE ( 'NONE', #6771, 8.400000000000000355 ) ;
#13306=EDGE_CURVE ( 'NONE', #159, #14739, #1028, .T. ) ;
#13312=EDGE_CURVE ( 'NONE', #6955, #5688, #12442, .T. ) ;
#13320=ORIENTED_EDGE ( 'NONE', *, *, #5772, .F. ) ;
#13331=CARTESIAN_POINT ( 'NONE',  ( 2.010451919658890585, -4.029281904976513395, -16.99607982911245330 ) ) ;
#13332=DIRECTION ( 'NONE',  ( 0.000000000000000000, 0.000000000000000000, 1.000000000000000000 ) ) ;
#13345=B_SPLINE_CURVE_WITH_KNOTS ( 'NONE', 3,
 ( #7302, #12121, #6219, #14683, #11972, #12209, #9758, #1460 ),
 .UNSPECIFIED., .F., .F.,
 ( 4, 2, 2, 4 ),
 ( 2.154797734452241992E-07, 0.001895231411414977432, 0.002842739377235738250, 0.003790247343056499067 ),
 .UNSPECIFIED. ) ;
#13347=DIRECTION ( 'NONE',  ( -1.000000000000000000, -0.000000000000000000, 0.000000000000000000 ) ) ;
#13353=ORIENTED_EDGE ( 'NONE', *, *, #13498, .T. ) ;
#13355=CIRCLE ( 'NONE', #11136, 2.524999999999999023 ) ;
#13358=ORIENTED_EDGE ( 'NONE', *, *, #14900, .F. ) ;
#13361=FACE_OUTER_BOUND ( 'NONE', #13187, .T. ) ;
#13362=CARTESIAN_POINT ( 'NONE',  ( 0.1920563539683076970, -15.58455734132164316, -2.883512197589173542 ) ) ;
#13365=AXIS2_PLACEMENT_3D ( 'NONE', #12272, #10963, #4056 ) ;
#13367=AXIS2_PLACEMENT_3D ( 'NONE', #7571, #10096, #12483 ) ;
#13373=CARTESIAN_POINT ( 'NONE',  ( 2.789999999999999147, 13.68080036884355621, -5.229914364928207604 ) ) ;
#13384=TOROIDAL_SURFACE ( 'NONE', #11171, 14.01039946648074341, 8.000000000000000000 ) ;
#13386=AXIS2_PLACEMENT_3D ( 'NONE', #6786, #13852, #5651 ) ;
#13397=FACE_OUTER_BOUND ( 'NONE', #11896, .T. ) ;
#13407=TOROIDAL_SURFACE ( 'NONE', #7766, 14.01039946648074341, 8.000000000000000000 ) ;
#13409=CIRCLE ( 'NONE', #10713, 17.95481323787947758 ) ;
#13412=CARTESIAN_POINT ( 'NONE',  ( 1.039999999999998037, 12.83329210556849276, -12.55714665599973756 ) ) ;
#13419=ORIENTED_EDGE ( 'NONE', *, *, #4717, .F. ) ;
#13428=AXIS2_PLACEMENT_3D ( 'NONE', #13287, #2841, #9988 ) ;
#13435=FACE_OUTER_BOUND ( 'NONE', #1988, .T. ) ;
#13438=AXIS2_PLACEMENT_3D ( 'NONE', #1745, #12189, #8651 ) ;
#13439=CARTESIAN_POINT ( 'NONE',  ( 0.5431870686475157584, -12.54666350726131618, 11.42270873787287933 ) ) ;
#13442=TOROIDAL_SURFACE ( 'NONE', #7812, 14.01039946648073986, 8.000000000000000000 ) ;
#13445=DIRECTION ( 'NONE',  ( -1.000000000000000000, -0.000000000000000000, -0.000000000000000000 ) ) ;
#13447=CARTESIAN_POINT ( 'NONE',  ( 2.764680872513688659, 2.311161484776556030, 14.46287784598618309 ) ) ;
#13449=AXIS2_PLACEMENT_3D ( 'NONE', #6885, #10638, #11564 ) ;
#13452=FACE_OUTER_BOUND ( 'NONE', #11653, .T. ) ;
#13456=VERTEX_POINT ( 'NONE', #9679 ) ;
#13463=VECTOR ( 'NONE', #12174, 1000.000000000000000 ) ;
#13467=DIRECTION ( 'NONE',  ( 0.000000000000000000, -0.4999999999999951705, -0.8660254037844413721 ) ) ;
#13468=FACE_OUTER_BOUND ( 'NONE', #2854, .T. ) ;
#13477=CARTESIAN_POINT ( 'NONE',  ( 2.764680872515354437, 13.68080036884355621, -5.229914364928207604 ) ) ;
#13478=ORIENTED_EDGE ( 'NONE', *, *, #10571, .T. ) ;
#13489=CIRCLE ( 'NONE', #1212, 17.95481323787947403 ) ;
#13490=CARTESIAN_POINT ( 'NONE',  ( 2.782650442329440921, -9.045126717605700861, -11.23191127083872942 ) ) ;
#13491=VERTEX_POINT ( 'NONE', #2221 ) ;
#13497=EDGE_CURVE ( 'NONE', #3044, #4505, #3948, .T. ) ;
#13498=EDGE_CURVE ( 'NONE', #7299, #12118, #8262, .T. ) ;
#13503=CARTESIAN_POINT ( 'NONE',  ( -9.947158122877977619E-15, 13.12804621868830957, -5.226330906375914687 ) ) ;
#13506=FACE_OUTER_BOUND ( 'NONE', #1670, .T. ) ;
#13511=DIRECTION ( 'NONE',  ( 0.000000000000000000, 0.000000000000000000, 1.000000000000000000 ) ) ;
#13518=ADVANCED_FACE ( 'NONE', ( #11430 ), #13684, .T. ) ;
#13522=ORIENTED_EDGE ( 'NONE', *, *, #4495, .F. ) ;
#13526=CARTESIAN_POINT ( 'NONE',  ( 2.789999999999999147, 8.624777288397954322, -11.04103753892262496 ) ) ;
#13530=B_SPLINE_CURVE_WITH_KNOTS ( 'NONE', 3,
 ( #765, #10141, #14832, #3230 ),
 .UNSPECIFIED., .F., .F.,
 ( 4, 4 ),
 ( 2.159563976928984569E-07, 0.0006916893629249152697 ),
 .UNSPECIFIED. ) ;
#13538=ORIENTED_EDGE ( 'NONE', *, *, #1484, .T. ) ;
#13540=AXIS2_PLACEMENT_3D ( 'NONE', #8932, #786, #12613 ) ;
#13543=CARTESIAN_POINT ( 'NONE',  ( 1.394999999999998685, 12.55714665599987079, 12.83329210556836308 ) ) ;
#13550=B_SPLINE_CURVE_WITH_KNOTS ( 'NONE', 3,
 ( #4814, #90, #8255, #9567, #11785, #3347, #2496, #2201 ),
 .UNSPECIFIED., .F., .F.,
 ( 4, 2, 2, 4 ),
 ( 2.445728210282435608E-07, 0.001895260649874691344, 0.002842768688401522276, 0.003790276726928352991 ),
 .UNSPECIFIED. ) ;
#13569=FACE_OUTER_BOUND ( 'NONE', #5083, .T. ) ;
#13572=ORIENTED_EDGE ( 'NONE', *, *, #13116, .T. ) ;
#13575=CARTESIAN_POINT ( 'NONE',  ( 0.02531912748679129854, 11.36963888406687317, 9.232963481057801403 ) ) ;
#13577=CARTESIAN_POINT ( 'NONE',  ( 0.1920562174424405855, -10.28947301956291049, 12.05486625177567994 ) ) ;
#13580=ORIENTED_EDGE ( 'NONE', *, *, #2445, .T. ) ;
#13589=ORIENTED_EDGE ( 'NONE', *, *, #1484, .F. ) ;
#13590=CARTESIAN_POINT ( 'NONE',  ( 0.7686372590627846835, 5.021526291670549647, -16.74220655292932136 ) ) ;
#13600=CARTESIAN_POINT ( 'NONE',  ( 2.740003288479521792, 14.75565684666127098, 2.439987328297021918 ) ) ;
#13608=ORIENTED_EDGE ( 'NONE', *, *, #2445, .F. ) ;
#13610=CARTESIAN_POINT ( 'NONE',  ( -10.00000000000000000, 0.000000000000000000, 0.000000000000000000 ) ) ;
#13611=CIRCLE ( 'NONE', #841, 14.01039946648073986 ) ;
#13612=EDGE_CURVE ( 'NONE', #8808, #1432, #12805, .T. ) ;
#13614=VECTOR ( 'NONE', #4161, 1000.000000000000000 ) ;
#13620=CYLINDRICAL_SURFACE ( 'NONE', #3877, 2.524999999999999467 ) ;
#13622=EDGE_CURVE ( 'NONE', #1439, #12007, #1001, .T. ) ;
#13628=CARTESIAN_POINT ( 'NONE',  ( 0.000000000000000000, 12.98979500319694225, 5.249430348645796940 ) ) ;
#13630=ORIENTED_EDGE ( 'NONE', *, *, #14002, .F. ) ;
#13635=DIRECTION ( 'NONE',  ( 0.000000000000000000, 0.000000000000000000, 1.000000000000000000 ) ) ;
#13641=EDGE_LOOP ( 'NONE', ( #1298, #874, #2523, #2397, #3940, #7909 ) ) ;
#13649=CARTESIAN_POINT ( 'NONE',  ( 2.700841271786576403, -14.29252738795474720, 5.279841123860291141 ) ) ;
#13650=AXIS2_PLACEMENT_3D ( 'NONE', #15150, #6066, #9522 ) ;
#13662=CIRCLE ( 'NONE', #9005, 14.01039946648073986 ) ;
#13676=CYLINDRICAL_SURFACE ( 'NONE', #1323, 17.95481323787947403 ) ;
#13678=AXIS2_PLACEMENT_3D ( 'NONE', #8952, #7887, #5374 ) ;
#13682=ORIENTED_EDGE ( 'NONE', *, *, #10218, .F. ) ;
#13684=TOROIDAL_SURFACE ( 'NONE', #5596, 14.01039946648074341, 8.000000000000000000 ) ;
#13686=CARTESIAN_POINT ( 'NONE',  ( 2.789999999999999147, -11.04103753892277417, 8.624777288397760699 ) ) ;
#13691=EDGE_CURVE ( 'NONE', #13251, #7858, #3018, .T. ) ;
#13695=ORIENTED_EDGE ( 'NONE', *, *, #13139, .F. ) ;
#13696=CARTESIAN_POINT ( 'NONE',  ( 2.337784053193427969, -12.42068120944088605, 11.13074453164198729 ) ) ;
#13700=CARTESIAN_POINT ( 'NONE',  ( 0.000000000000000000, -13.87420763704360382, -1.948757464274321949 ) ) ;
#13701=ORIENTED_EDGE ( 'NONE', *, *, #3452, .F. ) ;
#13704=EDGE_CURVE ( 'NONE', #3376, #1316, #5774, .T. ) ;
#13708=ADVANCED_FACE ( 'NONE', ( #1279 ), #2647, .T. ) ;
#13712=DIRECTION ( 'NONE',  ( 0.000000000000000000, 0.000000000000000000, 1.000000000000000000 ) ) ;
#13716=VERTEX_POINT ( 'NONE', #111 ) ;
#13721=DIRECTION ( 'NONE',  ( -1.000000000000000000, 0.000000000000000000, 0.000000000000000000 ) ) ;
#13722=CIRCLE ( 'NONE', #7590, 14.01039946648073986 ) ;
#13726=CARTESIAN_POINT ( 'NONE',  ( 0.01273908760111100436, -13.49730943211464762, -5.214906618940456262 ) ) ;
#13729=CARTESIAN_POINT ( 'NONE',  ( 2.789999999999999147, -11.07980565117287242, 9.999777909379893970 ) ) ;
#13733=AXIS2_PLACEMENT_3D ( 'NONE', #6860, #14942, #6779 ) ;
#13738=CARTESIAN_POINT ( 'NONE',  ( 0.7795480763126767521, -11.98750039041503257, 12.70439593876656481 ) ) ;
#13741=DIRECTION ( 'NONE',  ( -1.000000000000000000, -0.000000000000000000, -0.000000000000000000 ) ) ;
#13748=CARTESIAN_POINT ( 'NONE',  ( 0.000000000000000000, -12.98979500319690850, -5.249430348645889310 ) ) ;
#13749=ORIENTED_EDGE ( 'NONE', *, *, #6352, .T. ) ;
#13761=VERTEX_POINT ( 'NONE', #14439 ) ;
#13763=CARTESIAN_POINT ( 'NONE',  ( 2.789999999999999147, -1.948757464274269102, 13.87420763704360560 ) ) ;
#13770=ORIENTED_EDGE ( 'NONE', *, *, #5658, .T. ) ;
#13781=DIRECTION ( 'NONE',  ( 0.000000000000000000, 0.000000000000000000, -1.000000000000000000 ) ) ;
#13786=CARTESIAN_POINT ( 'NONE',  ( 1.039999999999997593, 0.000000000000000000, 0.000000000000000000 ) ) ;
#13788=EDGE_CURVE ( 'NONE', #12141, #10760, #14844, .T. ) ;
#13791=B_SPLINE_CURVE_WITH_KNOTS ( 'NONE', 3,
 ( #11464, #15014, #6636, #940 ),
 .UNSPECIFIED., .F., .F.,
 ( 4, 4 ),
 ( 0.005123742438166213088, 0.005540500595652342840 ),
 .UNSPECIFIED. ) ;
#13792=DIRECTION ( 'NONE',  ( -1.000000000000000000, 0.000000000000000000, 0.000000000000000000 ) ) ;
#13793=ORIENTED_EDGE ( 'NONE', *, *, #9236, .F. ) ;
#13803=FACE_OUTER_BOUND ( 'NONE', #5098, .T. ) ;
#13807=ADVANCED_FACE ( 'NONE', ( #5148 ), #349, .F. ) ;
#13813=CARTESIAN_POINT ( 'NONE',  ( 2.790000000000010694, -5.211150952915456713, 13.21889893246973635 ) ) ;
#13816=CARTESIAN_POINT ( 'NONE',  ( 2.789999999999999147, 0.000000000000000000, 0.000000000000000000 ) ) ;
#13825=CARTESIAN_POINT ( 'NONE',  ( 0.000000000000000000, -13.87420763704362869, 1.948757464274129214 ) ) ;
#13826=CARTESIAN_POINT ( 'NONE',  ( 8.000000000000000000, 0.000000000000000000, 0.000000000000000000 ) ) ;
#13828=ORIENTED_EDGE ( 'NONE', *, *, #309, .T. ) ;
#13830=CARTESIAN_POINT ( 'NONE',  ( 1.749999999999999778, 17.39253030560841395, 4.458161950358562109 ) ) ;
#13831=ORIENTED_EDGE ( 'NONE', *, *, #9986, .T. ) ;
#13836=( LENGTH_UNIT ( ) NAMED_UNIT ( * ) SI_UNIT ( .MILLI., .METRE. ) );
#13847=CARTESIAN_POINT ( 'NONE',  ( 0.2818303507154248932, 15.84037596932093273, -3.072260951847480825 ) ) ;
#13852=DIRECTION ( 'NONE',  ( -1.000000000000000000, -0.000000000000000000, -0.000000000000000000 ) ) ;
#13864=CARTESIAN_POINT ( 'NONE',  ( 2.603085161307575834, -14.83319344613228452, 5.279841123861228169 ) ) ;
#13870=PRODUCT_DEFINITION ( 'UNKNOWN', '', #67, #9786 ) ;
#13882=CARTESIAN_POINT ( 'NONE',  ( 1.885839517048286229, 4.239993951493212343, 17.20101185194002724 ) ) ;
#13887=DIRECTION ( 'NONE',  ( -1.000000000000000000, -0.000000000000000000, 0.000000000000000000 ) ) ;
#13892=CARTESIAN_POINT ( 'NONE',  ( 1.039999999999997593, 0.000000000000000000, 0.000000000000000000 ) ) ;
#13895=DIRECTION ( 'NONE',  ( 0.000000000000000000, 0.000000000000000000, 1.000000000000000000 ) ) ;
#13898=ORIENTED_EDGE ( 'NONE', *, *, #14754, .F. ) ;
#13899=B_SPLINE_CURVE_WITH_KNOTS ( 'NONE', 3,
 ( #5308, #12203, #5230, #362 ),
 .UNSPECIFIED., .F., .F.,
 ( 4, 4 ),
 ( 1.988537749986029444E-07, 0.0006916721208754052263 ),
 .UNSPECIFIED. ) ;
#13900=( GEOMETRIC_REPRESENTATION_CONTEXT ( 3 ) GLOBAL_UNCERTAINTY_ASSIGNED_CONTEXT ( ( #9925 ) ) GLOBAL_UNIT_ASSIGNED_CONTEXT ( ( #4169, #4005, #1855 ) ) REPRESENTATION_CONTEXT ( 'NONE', 'WORKASPACE' ) );
#13902=DIRECTION ( 'NONE',  ( -1.000000000000000000, -0.000000000000000000, -0.000000000000000000 ) ) ;
#13904=EDGE_CURVE ( 'NONE', #8235, #4803, #12418, .T. ) ;
#13905=CARTESIAN_POINT ( 'NONE',  ( -5.209999999999999964, 0.000000000000000000, 0.000000000000000000 ) ) ;
#13910=APPLICATION_CONTEXT ( 'automotive_design' ) ;
#13912=CARTESIAN_POINT ( 'NONE',  ( 2.789999999999999147, 11.36963888406700285, -9.232963481057645083 ) ) ;
#13935=EDGE_CURVE ( 'NONE', #6223, #516, #889, .T. ) ;
#13937=ORIENTED_EDGE ( 'NONE', *, *, #12204, .F. ) ;
#13942=ORIENTED_EDGE ( 'NONE', *, *, #7899, .F. ) ;
#13954=VERTEX_POINT ( 'NONE', #9270 ) ;
#13956=EDGE_CURVE ( 'NONE', #3683, #9176, #6597, .T. ) ;
#13958=CARTESIAN_POINT ( 'NONE',  ( -7.718536089453257173E-15, 8.842327429719251342, -11.12243880662604134 ) ) ;
#13961=CARTESIAN_POINT ( 'NONE',  ( 2.646101151981377075, 14.59528211759998406, 5.279841123860917307 ) ) ;
#13965=DIRECTION ( 'NONE',  ( -1.000000000000000000, 0.000000000000000000, 0.000000000000000000 ) ) ;
#13971=CARTESIAN_POINT ( 'NONE',  ( 1.039999999999997815, 17.29145405592688789, 4.835383649608532508 ) ) ;
#13973=ORIENTED_EDGE ( 'NONE', *, *, #14032, .F. ) ;
#13974=CIRCLE ( 'NONE', #9795, 17.95481323787947403 ) ;
#13984=CARTESIAN_POINT ( 'NONE',  ( 2.789999999999999147, -14.46287784598619020, 2.311161484776505404 ) ) ;
#13986=AXIS2_PLACEMENT_3D ( 'NONE', #13826, #14837, #14768 ) ;
#13987=EDGE_CURVE ( 'NONE', #6372, #132, #1263, .T. ) ;
#14002=EDGE_CURVE ( 'NONE', #6334, #12627, #4769, .T. ) ;
#14003=ORIENTED_EDGE ( 'NONE', *, *, #13704, .F. ) ;
#14008=PRODUCT ( 'short pitch roller chain wheel_s_iso_Chain wheel ISO - 12Z 05B-1 --12SA8.0N', 'short pitch roller chain wheel_s_iso_Chain wheel ISO - 12Z 05B-1 --12SA8.0N', '', ( #1903 ) ) ;
#14011=ORIENTED_EDGE ( 'NONE', *, *, #10218, .T. ) ;
#14025=CARTESIAN_POINT ( 'NONE',  ( 1.039999999999998037, -4.835383649608592904, 17.29145405592687368 ) ) ;
#14027=EDGE_CURVE ( 'NONE', #2567, #8808, #13550, .T. ) ;
#14031=CARTESIAN_POINT ( 'NONE',  ( 2.789999999999999147, 4.595504208220027920, 14.19996452731190750 ) ) ;
#14032=EDGE_CURVE ( 'NONE', #12400, #13089, #6329, .T. ) ;
#14043=CARTESIAN_POINT ( 'NONE',  ( -6.082681802200626239E-14, -13.12794558796726641, -5.226347720069425939 ) ) ;
#14045=DIRECTION ( 'NONE',  ( -1.000000000000000000, 0.000000000000000000, -0.000000000000000000 ) ) ;
#14050=CARTESIAN_POINT ( 'NONE',  ( 0.000000000000000000, 1.948757464274368578, -13.87420763704359494 ) ) ;
#14053=FACE_OUTER_BOUND ( 'NONE', #10425, .T. ) ;
#14063=EDGE_CURVE ( 'NONE', #6211, #9636, #530, .T. ) ;
#14064=CARTESIAN_POINT ( 'NONE',  ( 0.7795480827049480199, -5.008579424861446583, -16.73367785739762326 ) ) ;
#14069=B_SPLINE_CURVE_WITH_KNOTS ( 'NONE', 3,
 ( #8669, #373, #13362, #2842, #688, #11063, #14764, #4231 ),
 .UNSPECIFIED., .F., .F.,
 ( 4, 2, 2, 4 ),
 ( 2.154797737779156328E-07, 0.001895231411415139412, 0.002842739377235820215, 0.003790247343056500802 ),
 .UNSPECIFIED. ) ;
#14073=EDGE_CURVE ( 'NONE', #14197, #7731, #14416, .T. ) ;
#14080=ORIENTED_EDGE ( 'NONE', *, *, #9236, .T. ) ;
#14083=CARTESIAN_POINT ( 'NONE',  ( 0.02531912748631468327, -14.46287784598615644, -2.311161484776706576 ) ) ;
#14094=B_SPLINE_CURVE_WITH_KNOTS ( 'NONE', 3,
 ( #9319, #6486, #12606, #1010, #12684, #935, #3246, #4554 ),
 .UNSPECIFIED., .F., .F.,
 ( 4, 2, 2, 4 ),
 ( 4.663089342001531929E-07, 0.001898630032275743168, 0.002847711893946511599, 0.003796793755617280681 ),
 .UNSPECIFIED. ) ;
#14098=ORIENTED_EDGE ( 'NONE', *, *, #8893, .T. ) ;
#14099=DIRECTION ( 'NONE',  ( -1.000000000000000000, 0.000000000000000000, 0.000000000000000000 ) ) ;
#14104=CARTESIAN_POINT ( 'NONE',  ( 2.764680872515352661, 5.229914364928351489, 13.68080036884350292 ) ) ;
#14115=DIRECTION ( 'NONE',  ( 0.000000000000000000, 0.000000000000000000, 1.000000000000000000 ) ) ;
#14124=CARTESIAN_POINT ( 'NONE',  ( 0.02531912748606228100, -13.68080036884352246, 5.229914364928304416 ) ) ;
#14130=DIRECTION ( 'NONE',  ( 0.000000000000000000, 0.000000000000000000, 1.000000000000000000 ) ) ;
#14133=FACE_OUTER_BOUND ( 'NONE', #6231, .T. ) ;
#14145=DIRECTION ( 'NONE',  ( -1.000000000000000000, 0.000000000000000000, -0.000000000000000000 ) ) ;
#14146=CARTESIAN_POINT ( 'NONE',  ( 2.508169649284527569, -3.072260951847640698, 15.84037596932107483 ) ) ;
#14148=CARTESIAN_POINT ( 'NONE',  ( 0.1920563539683088072, -2.883512197589118475, 15.58455734132165560 ) ) ;
#14162=ORIENTED_EDGE ( 'NONE', *, *, #1857, .T. ) ;
#14171=EDGE_CURVE ( 'NONE', #10675, #8188, #14094, .T. ) ;
#14178=CARTESIAN_POINT ( 'NONE',  ( 2.764680872515354881, -13.68080036884352246, 5.229914364928304416 ) ) ;
#14187=CARTESIAN_POINT ( 'NONE',  ( 2.740003281797978474, 5.264737421541524576, 13.99876742897260939 ) ) ;
#14197=VERTEX_POINT ( 'NONE', #8086 ) ;
#14198=ORIENTED_EDGE ( 'NONE', *, *, #11681, .T. ) ;
#14211=CARTESIAN_POINT ( 'NONE',  ( 0.02531912748631555063, 2.311161484776756758, -14.46287784598614756 ) ) ;
#14218=AXIS2_PLACEMENT_3D ( 'NONE', #6815, #7039, #3574 ) ;
#14220=EDGE_CURVE ( 'NONE', #10087, #10003, #10616, .T. ) ;
#14222=ORIENTED_EDGE ( 'NONE', *, *, #8580, .F. ) ;
#14228=CARTESIAN_POINT ( 'NONE',  ( 2.337784053193427525, -11.13074453164194644, -12.42068120944093046 ) ) ;
#14230=EDGE_CURVE ( 'NONE', #4505, #13954, #7131, .T. ) ;
#14232=B_SPLINE_CURVE_WITH_KNOTS ( 'NONE', 3,
 ( #14290, #208, #4928, #9597, #3751, #1152, #8432, #13119 ),
 .UNSPECIFIED., .F., .F.,
 ( 4, 2, 2, 4 ),
 ( 2.445728210282408609E-07, 0.001895260649874690694, 0.002842768688401522276, 0.003790276726928353424 ),
 .UNSPECIFIED. ) ;
#14237=ORIENTED_EDGE ( 'NONE', *, *, #6101, .T. ) ;
#14246=DIRECTION ( 'NONE',  ( -1.000000000000000000, -0.000000000000000000, -0.000000000000000000 ) ) ;
#14252=CARTESIAN_POINT ( 'NONE',  ( 2.790000000000061320, -13.21862218141519563, 5.211197193340646017 ) ) ;
#14265=CARTESIAN_POINT ( 'NONE',  ( 2.789999999999999147, -1.948757464274269102, 13.87420763704360560 ) ) ;
#14268=CARTESIAN_POINT ( 'NONE',  ( 2.789999999999999147, -8.624777288397876163, 11.04103753892268713 ) ) ;
#14269=DIRECTION ( 'NONE',  ( -1.000000000000000000, 0.000000000000000000, 0.000000000000000000 ) ) ;
#14271=ORIENTED_EDGE ( 'NONE', *, *, #9777, .T. ) ;
#14276=CARTESIAN_POINT ( 'NONE',  ( 0.7686372158811272115, 11.98841295390598027, 12.71987259277439719 ) ) ;
#14277=CARTESIAN_POINT ( 'NONE',  ( 2.789999999999999147, 11.04103753892271556, 8.624777288397840636 ) ) ;
#14285=CYLINDRICAL_SURFACE ( 'NONE', #3056, 2.524999999999998579 ) ;
#14287=VERTEX_POINT ( 'NONE', #7394 ) ;
#14290=CARTESIAN_POINT ( 'NONE',  ( 0.02531912748679390063, 9.232963481057920418, -11.36963888406677725 ) ) ;
#14296=ORIENTED_EDGE ( 'NONE', *, *, #9336, .T. ) ;
#14301=CARTESIAN_POINT ( 'NONE',  ( 0.4522159373304741048, 16.32199768300079157, 3.429166897524482227 ) ) ;
#14304=CARTESIAN_POINT ( 'NONE',  ( 0.2076373213219097902, -2.899259574942639972, -15.57879356040266217 ) ) ;
#14314=LINE ( 'NONE', #12912, #2093 ) ;
#14323=VERTEX_POINT ( 'NONE', #5996 ) ;
#14327=CARTESIAN_POINT ( 'NONE',  ( 0.5537796877189847811, 12.52687487503418851, 11.41743294611079484 ) ) ;
#14328=EDGE_CURVE ( 'NONE', #10057, #6030, #10266, .T. ) ;
#14336=CARTESIAN_POINT ( 'NONE',  ( 0.02531912748631078014, -2.311161484776655950, 14.46287784598616355 ) ) ;
#14338=CARTESIAN_POINT ( 'NONE',  ( 0.000000000000000000, 0.000000000000000000, 0.000000000000000000 ) ) ;
#14344=CARTESIAN_POINT ( 'NONE',  ( 2.789999999999999147, 0.000000000000000000, 0.000000000000000000 ) ) ;
#14346=ADVANCED_FACE ( 'NONE', ( #4780 ), #9451, .F. ) ;
#14350=AXIS2_PLACEMENT_3D ( 'NONE', #10745, #7286, #2369 ) ;
#14359=FACE_OUTER_BOUND ( 'NONE', #6310, .T. ) ;
#14364=EDGE_CURVE ( 'NONE', #11164, #2043, #304, .T. ) ;
#14365=CIRCLE ( 'NONE', #12132, 14.01039946648074341 ) ;
#14370=EDGE_CURVE ( 'NONE', #132, #3713, #7675, .T. ) ;
#14372=CARTESIAN_POINT ( 'NONE',  ( 2.697960371751379149, -9.756102650610319671, 11.73065272960059602 ) ) ;
#14375=VERTEX_POINT ( 'NONE', #13222 ) ;
#14379=EDGE_CURVE ( 'NONE', #7299, #8724, #9044, .T. ) ;
#14384=CARTESIAN_POINT ( 'NONE',  ( 0.000000000000000000, -1.948757464274081030, -13.87420763704363580 ) ) ;
#14386=EDGE_LOOP ( 'NONE', ( #762, #590, #8920, #8061, #12095, #2923 ) ) ;
#14398=VECTOR ( 'NONE', #827, 1000.000000000000000 ) ;
#14402=CARTESIAN_POINT ( 'NONE',  ( -5.209999999999999964, 0.000000000000000000, 0.000000000000000000 ) ) ;
#14406=ORIENTED_EDGE ( 'NONE', *, *, #13060, .T. ) ;
#14409=FACE_OUTER_BOUND ( 'NONE', #8666, .T. ) ;
#14413=CARTESIAN_POINT ( 'NONE',  ( 0.02531912748606228100, -13.68080036884352246, 5.229914364928304416 ) ) ;
#14415=ORIENTED_EDGE ( 'NONE', *, *, #1277, .F. ) ;
#14416=LINE ( 'NONE', #14568, #14693 ) ;
#14439=CARTESIAN_POINT ( 'NONE',  ( 1.039999999999996927, 12.55714665600005375, -12.83329210556818545 ) ) ;
#14449=ORIENTED_EDGE ( 'NONE', *, *, #4677, .F. ) ;
#14458=CARTESIAN_POINT ( 'NONE',  ( 0.09203966225861301420, -15.03709480088673445, 2.583706482361980861 ) ) ;
#14464=CARTESIAN_POINT ( 'NONE',  ( 0.000000000000000000, -11.04103753892265871, -8.624777288397922348 ) ) ;
#14468=EDGE_CURVE ( 'NONE', #1007, #1420, #2334, .T. ) ;
#14470=CARTESIAN_POINT ( 'NONE',  ( 0.000000000000000000, 5.249430348645754307, 12.98979500319696534 ) ) ;
#14480=CARTESIAN_POINT ( 'NONE',  ( 0.000000000000000000, 8.624777288397805108, 11.04103753892274575 ) ) ;
#14482=CARTESIAN_POINT ( 'NONE',  ( 1.394999999999998685, -17.39253030560838198, -4.458161950358684678 ) ) ;
#14484=EDGE_CURVE ( 'NONE', #11577, #1894, #14069, .T. ) ;
#14489=AXIS2_PLACEMENT_3D ( 'NONE', #14673, #4215, #7741 ) ;
#14493=CARTESIAN_POINT ( 'NONE',  ( 0.04999670013151429060, 11.55877992729678638, -9.490919315500011777 ) ) ;
#14496=CARTESIAN_POINT ( 'NONE',  ( 2.597943565934061283, -14.93837896275546306, -5.295083827234870810 ) ) ;
#14498=ORIENTED_EDGE ( 'NONE', *, *, #13026, .F. ) ;
#14507=CYLINDRICAL_SURFACE ( 'NONE', #9870, 2.524999999999999467 ) ;
#14508=DIRECTION ( 'NONE',  ( 0.000000000000000000, 0.000000000000000000, 1.000000000000000000 ) ) ;
#14509=DIRECTION ( 'NONE',  ( -1.000000000000000000, -0.000000000000000000, -0.000000000000000000 ) ) ;
#14512=ORIENTED_EDGE ( 'NONE', *, *, #10826, .F. ) ;
#14527=ORIENTED_EDGE ( 'NONE', *, *, #4388, .T. ) ;
#14529=CARTESIAN_POINT ( 'NONE',  ( 1.039999999999997149, -17.39253030560844948, 4.458161950358441317 ) ) ;
#14535=CARTESIAN_POINT ( 'NONE',  ( 1.394999999999999574, -4.835383649608353984, -17.29145405592693763 ) ) ;
#14536=CARTESIAN_POINT ( 'NONE',  ( 0.02531912748464761401, -2.311161484776455222, -14.46287784598619908 ) ) ;
#14544=AXIS2_PLACEMENT_3D ( 'NONE', #5746, #15128, #4601 ) ;
#14547=ORIENTED_EDGE ( 'NONE', *, *, #6101, .F. ) ;
#14551=ORIENTED_EDGE ( 'NONE', *, *, #309, .F. ) ;
#14554=EDGE_LOOP ( 'NONE', ( #14296, #2447, #6907, #12336, #9915, #8236, #4062, #8494 ) ) ;
#14557=EDGE_CURVE ( 'NONE', #5808, #9595, #4001, .T. ) ;
#14562=CARTESIAN_POINT ( 'NONE',  ( 1.039999999999998037, 12.83329210556849276, -12.55714665599973756 ) ) ;
#14564=CARTESIAN_POINT ( 'NONE',  ( 0.1920564340659368097, 14.93837896275556609, -5.295083827234559060 ) ) ;
#14565=CYLINDRICAL_SURFACE ( 'NONE', #13367, 8.400000000000000355 ) ;
#14568=CARTESIAN_POINT ( 'NONE',  ( 1.394999999999999574, -12.55714665599996138, 12.83329210556827249 ) ) ;
#14574=ORIENTED_EDGE ( 'NONE', *, *, #9458, .F. ) ;
#14587=CARTESIAN_POINT ( 'NONE',  ( 2.337784068222783951, 5.191253194756234812, -15.84984805378626049 ) ) ;
#14589=DIRECTION ( 'NONE',  ( -1.000000000000000000, -0.000000000000000000, -0.000000000000000000 ) ) ;
#14592=CARTESIAN_POINT ( 'NONE',  ( 1.749999999999999778, -4.458161950358378256, -17.39253030560846369 ) ) ;
#14594=CARTESIAN_POINT ( 'NONE',  ( -5.209999999999999964, 0.000000000000000000, 0.000000000000000000 ) ) ;
#14598=EDGE_CURVE ( 'NONE', #4547, #8287, #498, .T. ) ;
#14600=CARTESIAN_POINT ( 'NONE',  ( 0.02531912748464718033, -14.46287784598619020, 2.311161484776505404 ) ) ;
#14602=ORIENTED_EDGE ( 'NONE', *, *, #6671, .F. ) ;
#14606=CARTESIAN_POINT ( 'NONE',  ( 2.789999999999999147, 1.948757464274172513, 13.87420763704361804 ) ) ;
#14607=CARTESIAN_POINT ( 'NONE',  ( 1.039999999999996483, 17.29145405592695539, -4.835383649608292700 ) ) ;
#14614=ORIENTED_EDGE ( 'NONE', *, *, #1277, .T. ) ;
#14622=EDGE_CURVE ( 'NONE', #8536, #8896, #13530, .T. ) ;
#14626=FACE_OUTER_BOUND ( 'NONE', #11106, .T. ) ;
#14628=FACE_OUTER_BOUND ( 'NONE', #3393, .T. ) ;
#14629=DIRECTION ( 'NONE',  ( 0.000000000000000000, 0.000000000000000000, 1.000000000000000000 ) ) ;
#14635=CARTESIAN_POINT ( 'NONE',  ( 2.789999999999999147, 7.739906618939707883, 13.40591150984229252 ) ) ;
#14636=CARTESIAN_POINT ( 'NONE',  ( 0.1869148386924337490, 14.83319344613230584, 5.279841123861332086 ) ) ;
#14639=VERTEX_POINT ( 'NONE', #13031 ) ;
#14642=CARTESIAN_POINT ( 'NONE',  ( 2.789999999999999147, -14.59528211760000005, 5.279841123860814278 ) ) ;
#14651=EDGE_CURVE ( 'NONE', #1007, #9176, #3590, .T. ) ;
#14658=ORIENTED_EDGE ( 'NONE', *, *, #3790, .T. ) ;
#14660=EDGE_CURVE ( 'NONE', #7166, #1439, #2368, .T. ) ;
#14670=CIRCLE ( 'NONE', #907, 17.95481323787947403 ) ;
#14673=CARTESIAN_POINT ( 'NONE',  ( 0.000000000000000000, 0.000000000000000000, 0.000000000000000000 ) ) ;
#14675=ORIENTED_EDGE ( 'NONE', *, *, #6921, .F. ) ;
#14679=EDGE_CURVE ( 'NONE', #367, #5551, #10526, .T. ) ;
#14683=CARTESIAN_POINT ( 'NONE',  ( 2.337784062669568730, 16.32199768300068499, -3.429166897524400071 ) ) ;
#14691=DIRECTION ( 'NONE',  ( 0.000000000000000000, -6.870191984066566880E-16, -1.000000000000000000 ) ) ;
#14693=VECTOR ( 'NONE', #4032, 1000.000000000000000 ) ;
#14697=CARTESIAN_POINT ( 'NONE',  ( 0.02531912748464674665, -11.36963888406694068, 9.232963481057725019 ) ) ;
#14700=DIRECTION ( 'NONE',  ( 1.000000000000000000, 0.000000000000000000, -0.000000000000000000 ) ) ;
#14702=B_SPLINE_CURVE_WITH_KNOTS ( 'NONE', 3,
 ( #8191, #5902, #12869, #33 ),
 .UNSPECIFIED., .F., .F.,
 ( 4, 4 ),
 ( 0.005123742438166227833, 0.005814376014856856636 ),
 .UNSPECIFIED. ) ;
#14703=ORIENTED_EDGE ( 'NONE', *, *, #13497, .F. ) ;
#14707=EDGE_CURVE ( 'NONE', #5314, #2246, #12973, .T. ) ;
#14710=TOROIDAL_SURFACE ( 'NONE', #4852, 14.01039946648074341, 8.000000000000000000 ) ;
#14711=AXIS2_PLACEMENT_3D ( 'NONE', #15048, #10058, #4219 ) ;
#14714=CYLINDRICAL_SURFACE ( 'NONE', #9556, 8.400000000000000355 ) ;
#14717=CARTESIAN_POINT ( 'NONE',  ( 2.789999999999999147, 0.000000000000000000, 0.000000000000000000 ) ) ;
#14718=CARTESIAN_POINT ( 'NONE',  ( 0.2393399843456231746, 15.07093484180037812, 5.269646308239136268 ) ) ;
#14721=ORIENTED_EDGE ( 'NONE', *, *, #4383, .F. ) ;
#14722=CARTESIAN_POINT ( 'NONE',  ( 0.01819315239479611657, 13.58898324715688588, -5.219858754686030444 ) ) ;
#14724=EDGE_LOOP ( 'NONE', ( #4335, #4092, #1996, #1241, #2838, #14721, #656 ) ) ;
#14726=DIRECTION ( 'NONE',  ( 1.000000000000000000, 0.000000000000000000, 0.000000000000000000 ) ) ;
#14739=VERTEX_POINT ( 'NONE', #7134 ) ;
#14744=CYLINDRICAL_SURFACE ( 'NONE', #1674, 2.524999999999999467 ) ;
#14751=ORIENTED_EDGE ( 'NONE', *, *, #9304, .T. ) ;
#14754=EDGE_CURVE ( 'NONE', #960, #10087, #3742, .T. ) ;
#14761=EDGE_LOOP ( 'NONE', ( #3685, #14658, #9469, #15135, #6766, #7093, #1261, #8212 ) ) ;
#14764=CARTESIAN_POINT ( 'NONE',  ( 0.9041604829517136954, -17.20101185193997395, -4.239993951493388202 ) ) ;
#14768=DIRECTION ( 'NONE',  ( 0.000000000000000000, 0.000000000000000000, 1.000000000000000000 ) ) ;
#14769=CARTESIAN_POINT ( 'NONE',  ( 2.789999999999999147, 7.739906618939895289, -13.40591150984218416 ) ) ;
#14774=ORIENTED_EDGE ( 'NONE', *, *, #12278, .F. ) ;
#14775=ORIENTED_EDGE ( 'NONE', *, *, #4968, .T. ) ;
#14780=CARTESIAN_POINT ( 'NONE',  ( 2.789999999999999147, 0.000000000000000000, 0.000000000000000000 ) ) ;
#14782=ORIENTED_EDGE ( 'NONE', *, *, #3317, .F. ) ;
#14784=FACE_OUTER_BOUND ( 'NONE', #14554, .T. ) ;
#14797=CARTESIAN_POINT ( 'NONE',  ( 2.789999999999999147, 12.98979500319694047, 5.249430348645800493 ) ) ;
#14799=CARTESIAN_POINT ( 'NONE',  ( 2.764680872513682441, -2.311161484776455222, -14.46287784598619908 ) ) ;
#14800=ORIENTED_EDGE ( 'NONE', *, *, #14468, .F. ) ;
#14807=CYLINDRICAL_SURFACE ( 'NONE', #12177, 8.400000000000000355 ) ;
#14810=VERTEX_POINT ( 'NONE', #1594 ) ;
#14812=DIRECTION ( 'NONE',  ( 1.000000000000000000, -0.000000000000000000, 0.000000000000000000 ) ) ;
#14813=FACE_OUTER_BOUND ( 'NONE', #5557, .T. ) ;
#14816=DIRECTION ( 'NONE',  ( -1.000000000000000000, 0.000000000000000000, 0.000000000000000000 ) ) ;
#14826=ORIENTED_EDGE ( 'NONE', *, *, #2598, .F. ) ;
#14831=CARTESIAN_POINT ( 'NONE',  ( 2.771806847605205792, -13.58898324715675976, -5.219858754686313773 ) ) ;
#14832=CARTESIAN_POINT ( 'NONE',  ( 2.790000000000061764, 2.096282088614963346, -14.05326139264725427 ) ) ;
#14837=DIRECTION ( 'NONE',  ( -1.000000000000000000, -0.000000000000000000, -0.000000000000000000 ) ) ;
#14838=CARTESIAN_POINT ( 'NONE',  ( 0.007327564474062031770, -9.044896821682122834, -11.23174270417338505 ) ) ;
#14841=CARTESIAN_POINT ( 'NONE',  ( 2.764680872515352217, 14.46287784598617243, 2.311161484776605324 ) ) ;
#14844=B_SPLINE_CURVE_WITH_KNOTS ( 'NONE', 3,
 ( #9818, #13503, #11954, #6130 ),
 .UNSPECIFIED., .F., .F.,
 ( 4, 4 ),
 ( 0.005123742438166223497, 0.005540500595652399218 ),
 .UNSPECIFIED. ) ;
#14846=EDGE_LOOP ( 'NONE', ( #6417, #3469, #10093, #4340 ) ) ;
#14852=AXIS2_PLACEMENT_3D ( 'NONE', #14996, #4386, #10443 ) ;
#14888=B_SPLINE_CURVE_WITH_KNOTS ( 'NONE', 3,
 ( #4211, #13649, #11412, #5516 ),
 .UNSPECIFIED., .F., .F.,
 ( 4, 4 ),
 ( 0.002880534149780641148, 0.003796793755617278946 ),
 .UNSPECIFIED. ) ;
#14892=CARTESIAN_POINT ( 'NONE',  ( 2.789999999999999147, 5.229914364928351489, 13.68080036884350292 ) ) ;
#14898=FACE_OUTER_BOUND ( 'NONE', #4751, .T. ) ;
#14900=EDGE_CURVE ( 'NONE', #1922, #14197, #14670, .T. ) ;
#14901=CARTESIAN_POINT ( 'NONE',  ( 2.789999999999999147, -9.232963481057685939, -11.36963888406697087 ) ) ;
#14906=DIRECTION ( 'NONE',  ( -1.000000000000000000, -0.000000000000000000, 0.000000000000000000 ) ) ;
#14916=DIRECTION ( 'NONE',  ( -1.000000000000000000, 0.000000000000000000, 0.000000000000000000 ) ) ;
#14919=CARTESIAN_POINT ( 'NONE',  ( 2.789999999999999147, -3.120158876138928505, -14.59528211760005334 ) ) ;
#14926=CARTESIAN_POINT ( 'NONE',  ( 2.782672467460655774, -2.217238903388661253, 14.24942254254688478 ) ) ;
#14931=EDGE_LOOP ( 'NONE', ( #535, #15095, #7490, #6884, #14003, #10151 ) ) ;
#14942=DIRECTION ( 'NONE',  ( -1.000000000000000000, -0.000000000000000000, -0.000000000000000000 ) ) ;
#14945=DIRECTION ( 'NONE',  ( 0.000000000000000000, 0.000000000000000000, 1.000000000000000000 ) ) ;
#14946=B_SPLINE_CURVE_WITH_KNOTS ( 'NONE', 3,
 ( #14536, #8670, #9684, #14384 ),
 .UNSPECIFIED., .F., .F.,
 ( 4, 4 ),
 ( 2.159563976372915910E-07, 0.0006916893629248553133 ),
 .UNSPECIFIED. ) ;
#14947=ADVANCED_FACE ( 'NONE', ( #13803 ), #812, .F. ) ;
#14953=FACE_OUTER_BOUND ( 'NONE', #7857, .T. ) ;
#14954=CARTESIAN_POINT ( 'NONE',  ( 2.790000000000008473, 11.12243880662625806, -8.842327429718979559 ) ) ;
#14964=AXIS2_PLACEMENT_3D ( 'NONE', #12344, #5299, #2907 ) ;
#14972=CARTESIAN_POINT ( 'NONE',  ( 0.000000000000000000, 1.948757464274177842, 13.87420763704361981 ) ) ;
#14973=TOROIDAL_SURFACE ( 'NONE', #13986, 14.01039946648074341, 8.000000000000000000 ) ;
#14996=CARTESIAN_POINT ( 'NONE',  ( 2.789999999999999147, 7.739906618939895289, -13.40591150984218416 ) ) ;
#14998=CARTESIAN_POINT ( 'NONE',  ( 2.646101151984011857, -14.59528211758545524, 5.279841123860813390 ) ) ;
#15007=ORIENTED_EDGE ( 'NONE', *, *, #8821, .T. ) ;
#15014=CARTESIAN_POINT ( 'NONE',  ( 2.790000000000011138, -13.12804621868818167, -5.226330906376194463 ) ) ;
#15047=ORIENTED_EDGE ( 'NONE', *, *, #9634, .T. ) ;
#15048=CARTESIAN_POINT ( 'NONE',  ( 2.789999999999999147, -13.40591150984221080, -7.739906618939849103 ) ) ;
#15056=ORIENTED_EDGE ( 'NONE', *, *, #12571, .T. ) ;
#15060=CARTESIAN_POINT ( 'NONE',  ( 2.715264205769513772, -15.04916547791956205, 2.569134216958844696 ) ) ;
#15087=CARTESIAN_POINT ( 'NONE',  ( 2.789999999999999147, -13.87420763704362514, 1.948757464274123885 ) ) ;
#15088=ADVANCED_FACE ( 'NONE', ( #5821 ), #12940, .T. ) ;
#15089=CARTESIAN_POINT ( 'NONE',  ( 0.09203966225857096450, 15.03709480088647865, -2.583706482361959100 ) ) ;
#15091=ORIENTED_EDGE ( 'NONE', *, *, #10599, .T. ) ;
#15095=ORIENTED_EDGE ( 'NONE', *, *, #10893, .F. ) ;
#15104=CARTESIAN_POINT ( 'NONE',  ( 2.789999999999999147, -5.229914364928447412, 13.68080036884346917 ) ) ;
#15109=CARTESIAN_POINT ( 'NONE',  ( 0.5537796532149702466, 3.624349476775427181, -16.55730827443876763 ) ) ;
#15117=CARTESIAN_POINT ( 'NONE',  ( 0.02531912748464718033, -9.232963481057685939, -11.36963888406697087 ) ) ;
#15128=DIRECTION ( 'NONE',  ( -1.000000000000000000, -0.000000000000000000, -0.000000000000000000 ) ) ;
#15129=CYLINDRICAL_SURFACE ( 'NONE', #11258, 8.400000000000000355 ) ;
#15134=CARTESIAN_POINT ( 'NONE',  ( 2.764680872513937349, -13.68080036884344963, -5.229914364928496262 ) ) ;
#15135=ORIENTED_EDGE ( 'NONE', *, *, #1503, .T. ) ;
#15137=CARTESIAN_POINT ( 'NONE',  ( 2.764680872513208598, 11.36963888406700285, -9.232963481057645083 ) ) ;
#15149=CIRCLE ( 'NONE', #4344, 4.000000000000000000 ) ;
#15150=CARTESIAN_POINT ( 'NONE',  ( -5.209999999999999964, 0.000000000000000000, 0.000000000000000000 ) ) ;
#15152=DIRECTION ( 'NONE',  ( -1.000000000000000000, 0.000000000000000000, -0.000000000000000000 ) ) ;
#15153=ORIENTED_EDGE ( 'NONE', *, *, #4859, .T. ) ;
#15154=CIRCLE ( 'NONE', #8502, 17.95481323787947403 ) ;
#15158=ORIENTED_EDGE ( 'NONE', *, *, #7230, .F. ) ;
#15159=ORIENTED_EDGE ( 'NONE', *, *, #12135, .T. ) ;
#15160=CARTESIAN_POINT ( 'NONE',  ( 1.394999999999998685, 4.835383649608714585, -17.29145405592683815 ) ) ;
#15163=CARTESIAN_POINT ( 'NONE',  ( 0.5431870686475157584, -11.42270873787283847, -12.54666350726135704 ) ) ;
#15167=CARTESIAN_POINT ( 'NONE',  ( 1.394999999999999574, -17.39253030560844593, 4.458161950358439540 ) ) ;
#15176=ORIENTED_EDGE ( 'NONE', *, *, #9410, .F. ) ;
#15179=EDGE_CURVE ( 'NONE', #12653, #3644, #4357, .T. ) ;
#15186=ORIENTED_EDGE ( 'NONE', *, *, #12909, .T. ) ;
#15191=DIRECTION ( 'NONE',  ( 0.000000000000000000, 0.000000000000000000, 1.000000000000000000 ) ) ;
#15192=AXIS2_PLACEMENT_3D ( 'NONE', #8862, #10028, #1881 ) ;
#15193=ORIENTED_EDGE ( 'NONE', *, *, #15214, .T. ) ;
#15207=DIRECTION ( 'NONE',  ( 0.000000000000000000, 0.000000000000000000, 1.000000000000000000 ) ) ;
#15208=CYLINDRICAL_SURFACE ( 'NONE', #7868, 2.524999999999999467 ) ;
#15214=EDGE_CURVE ( 'NONE', #6372, #4926, #7463, .T. ) ;
#15216=ORIENTED_EDGE ( 'NONE', *, *, #12185, .T. ) ;
#15220=ORIENTED_EDGE ( 'NONE', *, *, #5019, .T. ) ;
#15259=COLOUR_RGB('Sky Blue',0.24,0.69,0.87);
#15260=FILL_AREA_STYLE_COLOUR('',#15259);
#15261=FILL_AREA_STYLE('',(#15260));
#15262=SURFACE_STYLE_FILL_AREA(#15261);
#15263=SURFACE_SIDE_STYLE('',(#15262));
#15264=SURFACE_STYLE_USAGE(.BOTH.,#15263);
#15265=PRESENTATION_STYLE_ASSIGNMENT((#15264));
ENDSEC;
END-ISO-10303-21;
